ISO-10303-21;
HEADER;
/* Generated by software containing ST-Developer
 * from STEP Tools, Inc. (www.steptools.com) 
 */

FILE_DESCRIPTION(
/* description */ (''),
/* implementation_level */ '2;1');

FILE_NAME(
/* name */ 'Nut.step',
/* time_stamp */ '2026-10-04T22:13:49-07:00',
/* author */ (''),
/* organization */ (''),
/* preprocessor_version */ 'ST-DEVELOPER v20.2',
/* originating_system */ 'Autodesk Translation Framework v15.15.0.0',
/* authorisation */ '');

FILE_SCHEMA (('AUTOMOTIVE_DESIGN { 1 0 10303 214 3 1 1 }'));
ENDSEC;

DATA;
#10=MECHANICAL_DESIGN_GEOMETRIC_PRESENTATION_REPRESENTATION('',(#363),#40734);
#43=B_SPLINE_SURFACE_WITH_KNOTS('',3,3,((#5877,#5878,#5879,#5880,#5881,
#5882,#5883,#5884,#5885,#5886,#5887,#5888,#5889,#5890,#5891,#5892,#5893,
#5894,#5895,#5896,#5897,#5898,#5899,#5900),(#5901,#5902,#5903,#5904,#5905,
#5906,#5907,#5908,#5909,#5910,#5911,#5912,#5913,#5914,#5915,#5916,#5917,
#5918,#5919,#5920,#5921,#5922,#5923,#5924),(#5925,#5926,#5927,#5928,#5929,
#5930,#5931,#5932,#5933,#5934,#5935,#5936,#5937,#5938,#5939,#5940,#5941,
#5942,#5943,#5944,#5945,#5946,#5947,#5948),(#5949,#5950,#5951,#5952,#5953,
#5954,#5955,#5956,#5957,#5958,#5959,#5960,#5961,#5962,#5963,#5964,#5965,
#5966,#5967,#5968,#5969,#5970,#5971,#5972)),.UNSPECIFIED.,.F.,.F.,.F.,(4,
4),(4,1,1,1,1,1,1,1,1,1,1,1,1,1,1,1,1,1,1,1,1,4),(-0.000258182183401192,
0.0323763819078579),(11.855103081396,12.8491769023077,13.8429925410361,
14.8368081797645,15.8306238184928,16.8244394572212,17.8182550959496,18.8120707346779,
19.8058863734063,20.7997020121347,21.793517650863,22.7873332895914,23.7811489283198,
24.7749645670481,25.7687802057765,26.7625958445049,27.7564114832332,28.7502271219616,
29.74404276069,30.7378583994183,31.7316740381467,32.725489676875),
 .UNSPECIFIED.);
#44=B_SPLINE_SURFACE_WITH_KNOTS('',3,3,((#6139,#6140,#6141,#6142,#6143,
#6144,#6145,#6146,#6147,#6148,#6149,#6150,#6151,#6152,#6153,#6154,#6155,
#6156,#6157,#6158,#6159,#6160,#6161,#6162),(#6163,#6164,#6165,#6166,#6167,
#6168,#6169,#6170,#6171,#6172,#6173,#6174,#6175,#6176,#6177,#6178,#6179,
#6180,#6181,#6182,#6183,#6184,#6185,#6186),(#6187,#6188,#6189,#6190,#6191,
#6192,#6193,#6194,#6195,#6196,#6197,#6198,#6199,#6200,#6201,#6202,#6203,
#6204,#6205,#6206,#6207,#6208,#6209,#6210),(#6211,#6212,#6213,#6214,#6215,
#6216,#6217,#6218,#6219,#6220,#6221,#6222,#6223,#6224,#6225,#6226,#6227,
#6228,#6229,#6230,#6231,#6232,#6233,#6234)),.UNSPECIFIED.,.F.,.F.,.F.,(4,
4),(4,1,1,1,1,1,1,1,1,1,1,1,1,1,1,1,1,1,1,1,1,4),(-0.000227807970484936,
0.0323629493365531),(14.3984001269719,15.3922157657002,16.3860314044286,
17.379847043157,18.3736626818853,19.3674783206137,20.3612939593421,21.3551095980704,
22.3489252367988,23.3427408755272,24.3365565142555,25.3303721529839,26.3241877917123,
27.3180034304406,28.311819069169,29.3056347078974,30.2994503466257,31.2932659853541,
32.2870816240825,33.2808972628108,34.2747129015392,35.2685285402676),
 .UNSPECIFIED.);
#51=B_SPLINE_CURVE_WITH_KNOTS('',3,(#4121,#4122,#4123,#4124,#4125,#4126),
 .UNSPECIFIED.,.F.,.F.,(4,1,1,4),(30.4992669120821,30.7378583994183,31.7316740381467,
32.725489676875),.UNSPECIFIED.);
#52=B_SPLINE_CURVE_WITH_KNOTS('',3,(#4129,#4130,#4131,#4132,#4133,#4134,
#4135,#4136,#4137,#4138,#4139,#4140,#4141,#4142,#4143,#4144,#4145,#4146,
#4147,#4148,#4149,#4150,#4151,#4152,#4153,#4154,#4155,#4156,#4157,#4158,
#4159,#4160,#4161,#4162,#4163,#4164,#4165,#4166,#4167,#4168,#4169,#4170,
#4171,#4172,#4173,#4174,#4175,#4176,#4177,#4178,#4179,#4180,#4181,#4182,
#4183,#4184,#4185,#4186,#4187,#4188,#4189,#4190,#4191,#4192,#4193,#4194,
#4195,#4196,#4197,#4198,#4199,#4200,#4201,#4202,#4203,#4204),
 .UNSPECIFIED.,.F.,.F.,(4,3,3,3,3,3,3,3,3,3,3,3,3,3,3,3,3,3,3,3,3,3,3,3,
3,4),(30.5007322636873,30.6122727264591,30.7237376230315,30.8351702081999,
30.9496941524884,31.0612649927854,31.1772654890698,31.2932659853541,31.405444381662,
31.5174234643071,31.629291154361,31.7410902071455,31.8528632800448,31.9647326752084,
32.0766471573347,32.1887699843063,32.2870816240825,32.398548943329,32.5098233581226,
32.6209912335388,32.7320964774763,32.8431829042999,32.9543713853473,33.0656134824414,
33.1770570913779,33.2478062575977),.UNSPECIFIED.);
#53=B_SPLINE_CURVE_WITH_KNOTS('',3,(#4210,#4211,#4212,#4213,#4214,#4215,
#4216,#4217,#4218,#4219,#4220,#4221,#4222,#4223,#4224,#4225,#4226,#4227,
#4228,#4229,#4230,#4231,#4232,#4233,#4234,#4235,#4236,#4237,#4238,#4239,
#4240,#4241,#4242,#4243,#4244,#4245,#4246,#4247,#4248,#4249,#4250,#4251,
#4252,#4253,#4254,#4255,#4256,#4257,#4258,#4259,#4260,#4261,#4262,#4263,
#4264,#4265,#4266,#4267,#4268,#4269,#4270,#4271,#4272,#4273,#4274,#4275,
#4276,#4277,#4278,#4279,#4280,#4281,#4282,#4283,#4284,#4285,#4286,#4287,
#4288,#4289,#4290,#4291,#4292,#4293,#4294,#4295,#4296,#4297,#4298,#4299,
#4300,#4301,#4302,#4303,#4304,#4305,#4306,#4307,#4308,#4309,#4310,#4311,
#4312,#4313,#4314,#4315,#4316,#4317,#4318,#4319,#4320,#4321),
 .UNSPECIFIED.,.F.,.F.,(4,3,3,3,3,3,3,3,3,3,3,3,3,3,3,3,3,3,3,3,3,3,3,3,
3,3,3,3,3,3,3,3,3,3,3,3,3,4),(24.2171494664266,24.3287289861615,24.4404061429661,
24.5521266745184,24.6640652186713,24.7749645670481,24.8869176317094,24.9986729372709,
25.1103179593314,25.2218958291666,25.3334495814181,25.4451043023639,25.5568063273599,
25.668723124984,25.7687802057765,25.8807765547188,25.9925749208264,26.104262837802,
26.2158833658169,26.3274794682339,26.4391757243447,26.550918903972,26.6628756909807,
26.7625958445049,26.8745949120742,26.9863967358013,27.0980885559922,27.2097134207251,
27.3213142818085,27.4330159084715,27.5447648029427,27.6567278002384,27.7564114832332,
27.8729397438563,27.9891469003203,28.1051613568161,28.2209618754298,28.2743338823081),
 .UNSPECIFIED.);
#54=B_SPLINE_CURVE_WITH_KNOTS('',3,(#4322,#4323,#4324,#4325,#4326,#4327),
 .UNSPECIFIED.,.F.,.F.,(4,1,1,4),(28.2743354175824,28.7502271219616,29.74404276069,
30.4992669120821),.UNSPECIFIED.);
#55=B_SPLINE_CURVE_WITH_KNOTS('',3,(#4329,#4330,#4331,#4332,#4333,#4334,
#4335,#4336,#4337,#4338,#4339,#4340,#4341,#4342,#4343,#4344,#4345,#4346,
#4347,#4348,#4349,#4350,#4351,#4352,#4353,#4354,#4355,#4356,#4357,#4358,
#4359,#4360,#4361,#4362,#4363,#4364,#4365,#4366,#4367,#4368,#4369,#4370,
#4371,#4372,#4373,#4374,#4375,#4376,#4377,#4378,#4379,#4380,#4381,#4382,
#4383,#4384,#4385,#4386,#4387,#4388,#4389,#4390,#4391,#4392),
 .UNSPECIFIED.,.F.,.F.,(4,3,3,3,3,3,3,3,3,3,3,3,3,3,3,3,3,3,3,3,3,4),(28.2743338823081,
28.311819069169,28.4238155021246,28.5356139507129,28.6473019491837,28.7589225575854,
28.8705187391566,28.9822150718989,29.0939583268957,29.2059151862192,29.3056347078974,
29.4176340985753,29.5294362480819,29.6411283954428,29.7527535881624,29.8643547774776,
29.9760567301189,30.0878059498508,30.1997692670012,30.2994503466257,30.4112462518584,
30.5007322636873),.UNSPECIFIED.);
#56=B_SPLINE_CURVE_WITH_KNOTS('',3,(#4393,#4394,#4395,#4396,#4397,#4398,
#4399,#4400,#4401,#4402,#4403,#4404,#4405,#4406,#4407,#4408,#4409,#4410,
#4411,#4412,#4413,#4414,#4415,#4416,#4417,#4418,#4419,#4420,#4421,#4422,
#4423,#4424,#4425,#4426,#4427,#4428,#4429,#4430,#4431,#4432,#4433,#4434,
#4435,#4436,#4437,#4438,#4439,#4440,#4441,#4442,#4443,#4444,#4445,#4446,
#4447,#4448,#4449,#4450,#4451,#4452,#4453,#4454,#4455,#4456,#4457,#4458,
#4459,#4460,#4461,#4462,#4463,#4464,#4465,#4466,#4467,#4468,#4469,#4470,
#4471,#4472,#4473,#4474,#4475,#4476,#4477,#4478,#4479,#4480,#4481,#4482,
#4483,#4484,#4485,#4486,#4487,#4488,#4489,#4490,#4491,#4492,#4493,#4494,
#4495,#4496,#4497,#4498,#4499,#4500,#4501,#4502,#4503,#4504,#4505,#4506,
#4507),.UNSPECIFIED.,.F.,.F.,(4,3,3,3,3,3,3,3,3,3,3,3,3,3,3,3,3,3,3,3,3,
3,3,3,3,3,3,3,3,3,3,3,3,3,3,3,3,3,4),(24.2164788938612,24.3284578108245,
24.3365565142555,24.4485244285209,24.560294535519,24.6719543195167,24.7835468869861,
24.8951152477273,25.0067843218568,25.1185005830992,25.2304312375024,25.3303721529839,
25.4423485822127,25.5541272382699,25.6657955861649,25.7773967178561,25.8889736286533,
26.0006511630903,26.1123758489851,26.2243147601803,26.3241877917123,26.4361661670213,
26.5479468651215,26.6596173118309,26.7712205948806,26.8827997054225,26.9944794966149,
27.1062064741593,27.2181477050763,27.3180034304406,27.4292887012154,27.5403774827401,
27.651357678686,27.7622734955792,27.8731690428523,27.9841643917093,28.095212635599,
28.2064596772962,28.2743338817915),.UNSPECIFIED.);
#57=B_SPLINE_CURVE_WITH_KNOTS('',3,(#4513,#4514,#4515,#4516,#4517,#4518,
#4519,#4520,#4521,#4522,#4523,#4524,#4525,#4526,#4527,#4528,#4529,#4530,
#4531,#4532,#4533,#4534,#4535,#4536,#4537,#4538,#4539,#4540,#4541,#4542,
#4543,#4544,#4545,#4546,#4547,#4548,#4549,#4550,#4551,#4552,#4553,#4554,
#4555,#4556,#4557,#4558,#4559,#4560,#4561,#4562,#4563,#4564,#4565,#4566,
#4567,#4568,#4569,#4570,#4571,#4572,#4573),.UNSPECIFIED.,.F.,.F.,(4,3,3,
3,3,3,3,3,3,3,3,3,3,3,3,3,3,3,3,3,4),(15.707963267949,15.818355090934,15.9287111247549,
16.0430411946733,16.1535358156933,16.2697836100609,16.3860314044286,16.4981421037095,
16.6100544113457,16.7218559281154,16.8335894986427,16.9452978703484,17.0571042296374,
17.1689564942254,17.2810192004281,17.379847043157,17.4919974773912,17.6039638386448,
17.7158203932178,17.8276366370513,17.9335665904152),.UNSPECIFIED.);
#58=B_SPLINE_CURVE_WITH_KNOTS('',3,(#4575,#4576,#4577,#4578,#4579),
 .UNSPECIFIED.,.F.,.F.,(4,1,4),(14.3984001269719,15.3922157657002,15.7079548812379),
 .UNSPECIFIED.);
#59=B_SPLINE_CURVE_WITH_KNOTS('',3,(#4583,#4584,#4585,#4586,#4587,#4588,
#4589,#4590,#4591,#4592,#4593,#4594,#4595,#4596,#4597,#4598,#4599,#4600,
#4601,#4602,#4603,#4604,#4605,#4606,#4607,#4608,#4609,#4610,#4611,#4612,
#4613,#4614,#4615,#4616,#4617,#4618,#4619,#4620,#4621,#4622,#4623,#4624,
#4625,#4626,#4627,#4628,#4629,#4630,#4631,#4632,#4633,#4634),
 .UNSPECIFIED.,.F.,.F.,(4,3,3,3,3,3,3,3,3,3,3,3,3,3,3,3,3,4),(13.8759340267632,
13.9874055240017,14.0986819048936,14.2098503830277,14.3209548725418,14.4320391923179,
14.5432235672466,14.6544603986013,14.7658970889775,14.8368081797645,14.9473475531393,
15.0577376284281,15.1680237022244,15.2782509068263,15.3885311804989,15.4988322555113,
15.6093107358845,15.707963267949),.UNSPECIFIED.);
#60=B_SPLINE_CURVE_WITH_KNOTS('',3,(#4635,#4636,#4637,#4638,#4639,#4640,
#4641),.UNSPECIFIED.,.F.,.F.,(4,1,1,1,4),(15.707963267949,15.8306238184928,
16.8244394572212,17.8182550959496,17.9344079850994),.UNSPECIFIED.);
#61=B_SPLINE_CURVE_WITH_KNOTS('',3,(#4647,#4648,#4649,#4650,#4651,#4652,
#4653,#4654,#4655,#4656,#4657,#4658,#4659,#4660,#4661,#4662,#4663,#4664,
#4665,#4666,#4667,#4668,#4669,#4670,#4671,#4672,#4673,#4674,#4675,#4676,
#4677,#4678,#4679,#4680,#4681,#4682,#4683,#4684,#4685,#4686,#4687,#4688,
#4689,#4690,#4691,#4692,#4693,#4694,#4695,#4696,#4697,#4698),
 .UNSPECIFIED.,.F.,.F.,(4,3,3,3,3,3,3,3,3,3,3,3,3,3,3,3,3,4),(18.2326852175056,
18.3501141129404,18.4675228039056,18.5850446472557,18.7026282574228,18.8204305181141,
18.8824971358389,18.9989861703458,19.1152627236631,19.2314232752781,19.3475198007835,
19.4636041624104,19.5798208788147,19.6961099863659,19.8126414543351,19.8763127745673,
20.0320230471778,20.1591088879388),.UNSPECIFIED.);
#62=B_SPLINE_CURVE_WITH_KNOTS('',3,(#4700,#4701,#4702,#4703,#4704,#4705,
#4706,#4707,#4708,#4709,#4710,#4711,#4712,#4713),.UNSPECIFIED.,.F.,.F.,
(4,2,2,2,2,2,4),(-0.0902879860330804,-0.0695195013464431,-0.0576139772363393,
-0.0451609786697689,-0.0307684913612755,-0.00741601523602112,0.),
 .UNSPECIFIED.);
#63=B_SPLINE_CURVE_WITH_KNOTS('',3,(#4716,#4717,#4718,#4719,#4720,#4721,
#4722,#4723,#4724,#4725,#4726,#4727,#4728,#4729,#4730,#4731,#4732,#4733,
#4734,#4735,#4736,#4737,#4738,#4739,#4740,#4741,#4742,#4743,#4744,#4745,
#4746,#4747,#4748,#4749,#4750,#4751,#4752,#4753,#4754,#4755,#4756,#4757,
#4758,#4759,#4760,#4761,#4762,#4763,#4764,#4765,#4766,#4767,#4768,#4769,
#4770,#4771,#4772,#4773,#4774,#4775,#4776,#4777,#4778,#4779,#4780,#4781,
#4782,#4783,#4784,#4785,#4786,#4787,#4788,#4789,#4790,#4791,#4792,#4793,
#4794,#4795,#4796,#4797),.UNSPECIFIED.,.F.,.F.,(4,2,2,2,2,2,2,2,2,2,2,2,
2,2,2,2,2,2,2,2,2,2,2,2,2,2,2,2,2,2,2,2,2,2,2,2,2,2,2,2,4),(-1.10310963530152,
-1.09840428209197,-1.07722214007663,-1.06150851698653,-1.04868281780305,
-1.03819235320156,-1.02138418259208,-0.999282379625926,-0.990602595865436,
-0.983495936132868,-0.976570972649354,-0.961692691255592,-0.940952466821429,
-0.926313970937883,-0.916002211406824,-0.902436796120762,-0.870391217176744,
-0.860477072002617,-0.854465023776041,-0.845070439673182,-0.819245833374607,
-0.806702496780286,-0.79543475800065,-0.784817093076859,-0.762133674934839,
-0.745228751131369,-0.734731689538218,-0.728719271759347,-0.719808072857297,
-0.694096875566972,-0.681109182806924,-0.669588324732776,-0.658941721449021,
-0.638880453131988,-0.614447417440931,-0.606635107300723,-0.600344143431757,
-0.588300966408003,-0.564446554319691,-0.552834380572,-0.552725405623167),
 .UNSPECIFIED.);
#64=B_SPLINE_CURVE_WITH_KNOTS('',3,(#4803,#4804,#4805,#4806,#4807,#4808,
#4809,#4810,#4811,#4812,#4813,#4814,#4815,#4816,#4817,#4818,#4819,#4820,
#4821,#4822,#4823,#4824,#4825,#4826,#4827,#4828,#4829,#4830,#4831,#4832,
#4833,#4834,#4835,#4836,#4837,#4838,#4839,#4840,#4841,#4842,#4843,#4844,
#4845,#4846,#4847,#4848,#4849,#4850,#4851,#4852,#4853,#4854,#4855,#4856,
#4857),.UNSPECIFIED.,.F.,.F.,(4,3,3,3,3,3,3,3,3,3,3,3,3,3,3,3,3,3,4),(11.9491877790605,
12.0704897196116,12.1879350799606,12.3052738059049,12.4225558808697,12.539831191545,
12.6572286481437,12.7747004780911,12.892380281892,12.9196033034688,13.0391446098747,
13.1558912766851,13.2725228710644,13.3890907032798,13.5108014661389,13.6274735002162,
13.7442192750413,13.8611645569831,13.8759337547162),.UNSPECIFIED.);
#65=B_SPLINE_CURVE_WITH_KNOTS('',3,(#4858,#4859,#4860,#4861,#4862,#4863,
#4864,#4865,#4866,#4867,#4868,#4869,#4870,#4871,#4872,#4873,#4874,#4875,
#4876,#4877,#4878,#4879,#4880,#4881,#4882,#4883,#4884,#4885,#4886,#4887,
#4888,#4889,#4890,#4891,#4892,#4893,#4894,#4895,#4896,#4897,#4898,#4899,
#4900,#4901,#4902,#4903,#4904,#4905,#4906,#4907,#4908,#4909,#4910,#4911,
#4912,#4913,#4914,#4915,#4916,#4917,#4918,#4919,#4920,#4921,#4922,#4923,
#4924,#4925,#4926,#4927,#4928,#4929,#4930,#4931,#4932,#4933,#4934,#4935,
#4936,#4937,#4938,#4939,#4940,#4941,#4942,#4943,#4944,#4945,#4946,#4947,
#4948,#4949,#4950,#4951,#4952,#4953,#4954,#4955,#4956,#4957,#4958,#4959,
#4960,#4961,#4962,#4963,#4964,#4965,#4966,#4967,#4968,#4969,#4970,#4971,
#4972,#4973,#4974,#4975,#4976,#4977,#4978),.UNSPECIFIED.,.F.,.F.,(4,3,3,
3,3,3,3,3,3,3,3,3,3,3,3,3,3,3,3,3,3,3,3,3,3,3,3,3,3,3,3,3,3,3,3,3,3,3,3,
3,4),(13.8759337553363,13.9134189421971,14.0311296480262,14.1486252389434,
14.2660024664715,14.383311313252,14.5006016500783,14.6180056712398,14.735473475376,
14.8531565546079,14.9072345809255,15.0249483953848,15.1424479004606,15.2598295359287,
15.377143269917,15.4944389593616,15.6118489804661,15.7293231625642,15.8470131172698,
15.9010502196539,16.0185862160695,16.1359071716103,16.2531099559165,16.3702448724762,
16.4873621130608,16.604595636191,16.7218941812094,16.8394118468141,16.8948658583822,
17.0127678116824,17.1304532100569,17.2480191781504,17.365515344718,17.4829912252123,
17.6005766740717,17.7182237949846,17.8360809197351,17.8886814971106,18.006475161737,
18.1240829762214,18.2326852175056),.UNSPECIFIED.);
#66=B_SPLINE_CURVE_WITH_KNOTS('',3,(#4980,#4981,#4982,#4983,#4984,#4985,
#4986,#4987,#4988,#4989,#4990,#4991,#4992,#4993,#4994,#4995,#4996,#4997,
#4998,#4999,#5000,#5001,#5002,#5003,#5004,#5005,#5006,#5007,#5008,#5009,
#5010,#5011,#5012,#5013,#5014,#5015,#5016,#5017,#5018,#5019,#5020,#5021,
#5022,#5023,#5024,#5025,#5026,#5027,#5028,#5029,#5030,#5031,#5032,#5033,
#5034,#5035,#5036,#5037,#5038,#5039,#5040,#5041,#5042,#5043,#5044,#5045,
#5046,#5047,#5048,#5049,#5050,#5051,#5052,#5053,#5054,#5055,#5056,#5057,
#5058,#5059),.UNSPECIFIED.,.F.,.F.,(4,2,2,2,2,2,2,2,2,2,2,2,2,2,2,2,2,2,
2,2,2,2,2,2,2,2,2,2,2,2,2,2,2,2,2,2,2,2,2,4),(-0.552725405623167,-0.541977170966905,
-0.53084957666005,-0.51866977594079,-0.490571100145663,-0.481793473449696,
-0.475745498289177,-0.464874554957004,-0.446785851085663,-0.425816502562416,
-0.415167087894251,-0.403760289275286,-0.390983977795993,-0.365216310304077,
-0.356082527804832,-0.35005340954438,-0.33973200687133,-0.323398146844299,
-0.299824069413248,-0.289158384786419,-0.277737870662131,-0.264943180238732,
-0.233016973059306,-0.226580840545827,-0.219169303547567,-0.209851774465103,
-0.182807487580695,-0.169162145546328,-0.158906935173509,-0.144586539612125,
-0.124772548138701,-0.107597516249468,-0.10099011512184,-0.0938729126324881,
-0.0851219325742436,-0.0624426869455938,-0.0456861069530859,-0.0353317986472908,
-0.0229676387407706,-0.00036925595930691),.UNSPECIFIED.);
#67=B_SPLINE_CURVE_WITH_KNOTS('',3,(#5060,#5061,#5062,#5063,#5064,#5065,
#5066,#5067,#5068,#5069,#5070,#5071,#5072,#5073,#5074,#5075,#5076,#5077,
#5078,#5079,#5080,#5081,#5082,#5083,#5084,#5085,#5086,#5087,#5088,#5089,
#5090,#5091,#5092,#5093,#5094,#5095,#5096,#5097,#5098,#5099,#5100,#5101,
#5102,#5103,#5104,#5105,#5106,#5107,#5108,#5109,#5110,#5111,#5112,#5113,
#5114),.UNSPECIFIED.,.F.,.F.,(4,3,3,3,3,3,3,3,3,3,3,3,3,3,3,3,3,3,4),(-10.1357873115492,
-9.96754509954774,-9.93815638728366,-9.82046673168105,-9.70299196205392,
-9.58563539619237,-9.46834701434813,-9.35107690841475,-9.23369261088505,
-9.11624426811025,-8.99858002714185,-8.94434074855529,-8.82667899846583,
-8.7091951599211,-8.59183899812951,-8.47453671765872,-8.35726362182951,
-8.23992726492522,-8.20946475857041),.UNSPECIFIED.);
#68=B_SPLINE_CURVE_WITH_KNOTS('',3,(#5120,#5121,#5122,#5123,#5124,#5125,
#5126,#5127,#5128,#5129,#5130,#5131,#5132,#5133,#5134,#5135,#5136,#5137,
#5138,#5139,#5140,#5141,#5142,#5143,#5144,#5145,#5146,#5147,#5148,#5149,
#5150,#5151,#5152,#5153,#5154,#5155,#5156,#5157,#5158,#5159,#5160,#5161,
#5162,#5163,#5164,#5165,#5166,#5167,#5168,#5169,#5170,#5171),
 .UNSPECIFIED.,.F.,.F.,(4,3,3,3,3,3,3,3,3,3,3,3,3,3,3,3,3,4),(-1.9253726413955,
-1.80892801606211,-1.69271607294993,-1.57659231075127,-1.46050482883161,
-1.3438325313058,-1.22757869284794,-1.11069716578816,-0.993815638728368,
-0.869588683887322,-0.748964684319401,-0.628496931294659,-0.508144556691677,
-0.387866877787889,-0.267588204475049,-0.147310085942533,-0.0269467534811709,
0.),.UNSPECIFIED.);
#69=B_SPLINE_CURVE_WITH_KNOTS('',3,(#5174,#5175,#5176,#5177,#5178,#5179,
#5180,#5181,#5182,#5183,#5184,#5185,#5186,#5187,#5188,#5189,#5190,#5191,
#5192,#5193,#5194,#5195,#5196,#5197,#5198,#5199,#5200,#5201,#5202,#5203,
#5204,#5205,#5206,#5207,#5208,#5209,#5210,#5211,#5212,#5213,#5214,#5215,
#5216,#5217,#5218,#5219,#5220,#5221,#5222,#5223,#5224,#5225,#5226,#5227,
#5228,#5229,#5230,#5231,#5232,#5233,#5234,#5235,#5236,#5237,#5238,#5239,
#5240,#5241,#5242,#5243,#5244,#5245,#5246,#5247,#5248,#5249,#5250,#5251,
#5252,#5253,#5254,#5255,#5256,#5257,#5258,#5259,#5260,#5261,#5262,#5263,
#5264,#5265,#5266,#5267,#5268,#5269,#5270,#5271,#5272,#5273),
 .UNSPECIFIED.,.F.,.F.,(4,3,3,3,3,3,3,3,3,3,3,3,3,3,3,3,3,3,3,3,3,3,3,3,
3,3,3,3,3,3,3,3,3,4),(2.02058586035984,2.140693492338,2.25763871850387,
2.37446977250673,2.49123762200474,2.61378994554983,2.73066277291718,2.84760915246737,
2.96475566751446,2.9814469161851,3.09932762598598,3.21699987894726,3.33455773188,
3.45205079961854,3.56952859030924,3.68712343907614,3.8047842612984,3.9226614896851,
3.97526255491346,4.09280623566134,4.21013195125936,4.32733768164007,4.44447373540583,
4.56159030700783,4.67882045378987,4.79611407133702,4.91362448723962,4.96907819364183,
5.08676714789316,5.20427682387841,5.32166915676348,5.43898696672328,5.55634477834659,
5.66535571352405),.UNSPECIFIED.);
#70=B_SPLINE_CURVE_WITH_KNOTS('',3,(#5276,#5277,#5278,#5279,#5280,#5281,
#5282,#5283,#5284,#5285,#5286,#5287,#5288,#5289,#5290,#5291,#5292,#5293,
#5294,#5295,#5296,#5297,#5298,#5299,#5300,#5301,#5302,#5303,#5304,#5305,
#5306,#5307,#5308,#5309,#5310,#5311,#5312,#5313,#5314,#5315,#5316,#5317,
#5318,#5319,#5320,#5321,#5322,#5323,#5324,#5325,#5326,#5327,#5328,#5329,
#5330),.UNSPECIFIED.,.F.,.F.,(4,3,3,3,3,3,3,3,3,3,3,3,3,3,3,3,3,3,4),(5.66535571352405,
5.78282313787065,5.90050854996624,5.9628938323702,6.08060184387462,6.19809576663304,
6.31547196297819,6.43278041377381,6.55007098888068,6.66747619791458,6.78494573459987,
6.90263135953802,6.95670947109856,7.07492583639565,7.19294503118885,7.31080723912486,
7.42857851003219,7.54632867482091,7.59274844815668),.UNSPECIFIED.);
#71=B_SPLINE_CURVE_WITH_KNOTS('',3,(#5331,#5332,#5333,#5334,#5335,#5336,
#5337,#5338,#5339,#5340,#5341,#5342,#5343,#5344,#5345,#5346,#5347,#5348,
#5349,#5350,#5351,#5352,#5353,#5354,#5355,#5356,#5357,#5358,#5359,#5360,
#5361,#5362,#5363,#5364,#5365,#5366,#5367,#5368,#5369,#5370,#5371,#5372,
#5373,#5374,#5375,#5376,#5377,#5378,#5379,#5380,#5381,#5382,#5383,#5384,
#5385,#5386,#5387,#5388,#5389,#5390,#5391,#5392,#5393,#5394,#5395,#5396,
#5397,#5398,#5399,#5400,#5401,#5402,#5403,#5404,#5405,#5406,#5407,#5408,
#5409,#5410,#5411,#5412,#5413,#5414,#5415,#5416,#5417,#5418,#5419,#5420,
#5421,#5422,#5423,#5424,#5425,#5426,#5427,#5428,#5429,#5430,#5431,#5432,
#5433,#5434,#5435,#5436,#5437,#5438,#5439,#5440,#5441,#5442,#5443,#5444,
#5445,#5446,#5447,#5448,#5449,#5450,#5451),.UNSPECIFIED.,.F.,.F.,(4,3,3,
3,3,3,3,3,3,3,3,3,3,3,3,3,3,3,3,3,3,3,3,3,3,3,3,3,3,3,3,3,3,3,3,3,3,3,3,
3,4),(7.59274844890258,7.72609722425204,7.86061502881771,7.95052510982693,
8.06821691258659,8.18569390433419,8.30305273661296,8.42034342427409,8.53761587058653,
8.65500254100594,8.77245327853699,8.89011991932543,8.94434074855529,9.06203010323196,
9.17950469623869,9.29686116261319,9.41414952184228,9.53141968187335,9.64880414817428,
9.76625272552297,9.88391729904848,9.93815638728366,10.0558371193437,10.1733029282768,
10.2906505181704,10.4079299255747,10.5251910753747,10.6425665139707,10.760006040877,
10.8776616330052,10.931972026012,11.0496617074852,11.1671365028361,11.2844930943089,
11.4017815016062,11.5190516327888,11.636435955069,11.7538843223442,11.8715485871527,
11.9257876647404,11.9491877790605),.UNSPECIFIED.);
#72=B_SPLINE_CURVE_WITH_KNOTS('',3,(#5453,#5454,#5455,#5456,#5457,#5458,
#5459,#5460,#5461,#5462,#5463,#5464,#5465,#5466,#5467,#5468,#5469,#5470,
#5471,#5472,#5473,#5474,#5475,#5476,#5477,#5478,#5479,#5480,#5481,#5482,
#5483,#5484,#5485,#5486,#5487,#5488,#5489,#5490,#5491,#5492,#5493,#5494,
#5495,#5496,#5497,#5498,#5499,#5500,#5501,#5502,#5503,#5504,#5505,#5506,
#5507,#5508,#5509,#5510,#5511,#5512,#5513,#5514,#5515,#5516,#5517,#5518,
#5519,#5520,#5521,#5522,#5523,#5524,#5525,#5526,#5527,#5528,#5529,#5530,
#5531,#5532,#5533,#5534,#5535,#5536,#5537,#5538,#5539,#5540,#5541,#5542,
#5543,#5544,#5545,#5546,#5547,#5548,#5549,#5550,#5551,#5552,#5553,#5554,
#5555,#5556,#5557,#5558,#5559,#5560,#5561,#5562,#5563,#5564,#5565,#5566,
#5567,#5568,#5569,#5570,#5571,#5572,#5573),.UNSPECIFIED.,.F.,.F.,(4,3,3,
3,3,3,3,3,3,3,3,3,3,3,3,3,3,3,3,3,3,3,3,3,3,3,3,3,3,3,3,3,3,3,3,3,3,3,3,
3,4),(-8.20946475857041,-8.09199014784659,-7.97430853604256,-7.95052510982693,
-7.8328599850263,-7.7154097312376,-7.59807765075524,-7.48081367822952,-7.36356785992191,
-7.24620747770174,-7.12878287120506,-7.01114181960341,-6.95670947109856,
-6.83899885356979,-6.7215033492923,-6.60412620730503,-6.48681744482345,
-6.36952719090972,-6.25212324996335,-6.13465552461373,-6.01697252110421,
-5.9628938323702,-5.84518035750499,-5.7276811949198,-5.61029990342987,-5.49298651424117,
-5.37569116975381,-5.25828149111712,-5.1408076505398,-5.02311803196177,
-4.96907819364183,-4.85154138746856,-4.73421962199873,-4.6170160282861,
-4.49988030427019,-4.38276225960712,-4.26552794359781,-4.14822861091272,
-4.0307101746435,-3.97526255491346,-3.85260200436959),.UNSPECIFIED.);
#73=B_SPLINE_CURVE_WITH_KNOTS('',3,(#5574,#5575,#5576,#5577,#5578,#5579,
#5580,#5581,#5582,#5583,#5584,#5585,#5586,#5587,#5588,#5589,#5590,#5591,
#5592,#5593,#5594,#5595,#5596,#5597,#5598,#5599,#5600,#5601,#5602,#5603,
#5604,#5605,#5606,#5607,#5608,#5609,#5610,#5611,#5612,#5613,#5614,#5615,
#5616,#5617,#5618,#5619,#5620,#5621,#5622,#5623,#5624,#5625,#5626,#5627,
#5628),.UNSPECIFIED.,.F.,.F.,(4,3,3,3,3,3,3,3,3,3,3,3,3,3,3,3,3,3,4),(-3.85260200386407,
-3.73648747745417,-3.62051638895482,-3.50463624099859,-3.38879469763866,
-3.27286091253272,-3.15687669525244,-3.04068630600158,-2.9814469161851,
-2.86363061157218,-2.74602508039629,-2.62853533549447,-2.51111164876292,
-2.39370440056642,-2.27618134800846,-2.15859314055966,-2.04078899997219,
-1.98763127745673,-1.9253726413955),.UNSPECIFIED.);
#74=B_SPLINE_CURVE_WITH_KNOTS('',3,(#5631,#5632,#5633,#5634,#5635,#5636,
#5637,#5638),.UNSPECIFIED.,.F.,.F.,(4,1,1,1,1,4),(17.9344079850994,18.8120707346779,
19.8058863734063,20.7997020121347,21.793517650863,21.9911485751285),
 .UNSPECIFIED.);
#75=B_SPLINE_CURVE_WITH_KNOTS('',3,(#5639,#5640,#5641,#5642,#5643,#5644,
#5645,#5646,#5647,#5648,#5649,#5650,#5651,#5652,#5653,#5654,#5655,#5656,
#5657,#5658,#5659,#5660,#5661,#5662,#5663,#5664,#5665,#5666,#5667,#5668,
#5669,#5670,#5671,#5672,#5673,#5674,#5675,#5676,#5677,#5678,#5679,#5680,
#5681,#5682,#5683,#5684,#5685,#5686,#5687,#5688,#5689,#5690,#5691,#5692,
#5693,#5694,#5695,#5696,#5697,#5698,#5699,#5700,#5701,#5702),
 .UNSPECIFIED.,.F.,.F.,(4,3,3,3,3,3,3,3,3,3,3,3,3,3,3,3,3,3,3,3,3,4),(21.9911485751285,
22.1012980243391,22.2113482880773,22.321344734747,22.4313326401807,22.5414276972775,
22.6515882903729,22.7619346601458,22.7873332895914,22.8993096942055,23.0110883257836,
23.1227566492983,23.2343577567475,23.3459346434801,23.4576121543163,23.5693368168269,
23.6812757052973,23.7811489283198,23.8930884987303,24.0048748237804,24.1165488904639,
24.2171494664266),.UNSPECIFIED.);
#76=B_SPLINE_CURVE_WITH_KNOTS('',3,(#5704,#5705,#5706,#5707,#5708,#5709,
#5710,#5711,#5712,#5713,#5714,#5715,#5716,#5717,#5718,#5719,#5720,#5721,
#5722,#5723,#5724,#5725,#5726,#5727,#5728,#5729,#5730,#5731,#5732,#5733,
#5734,#5735,#5736,#5737,#5738,#5739,#5740,#5741,#5742,#5743,#5744,#5745,
#5746,#5747,#5748,#5749,#5750,#5751,#5752,#5753,#5754,#5755,#5756,#5757,
#5758,#5759,#5760,#5761,#5762,#5763,#5764),.UNSPECIFIED.,.F.,.F.,(4,3,3,
3,3,3,3,3,3,3,3,3,3,3,3,3,3,3,3,3,4),(21.9911485755794,22.1180239270845,
22.2459913725795,22.3489252367988,22.4609036843361,22.5726844279904,22.684354904006,
22.7959582001587,22.9075373076252,23.0192170705217,23.1309440058854,23.2428851718823,
23.3427408755272,23.4546781603108,23.5664579396098,23.6781234690952,23.7897178493381,
23.9013376620179,24.0129645371053,24.1247338172087,24.2164788938612),
 .UNSPECIFIED.);
#77=B_SPLINE_CURVE_WITH_KNOTS('',3,(#5765,#5766,#5767,#5768,#5769,#5770,
#5771,#5772,#5773,#5774,#5775,#5776,#5777,#5778,#5779,#5780,#5781,#5782,
#5783,#5784,#5785,#5786,#5787,#5788,#5789,#5790,#5791,#5792,#5793,#5794,
#5795,#5796,#5797,#5798,#5799,#5800,#5801,#5802,#5803,#5804,#5805,#5806,
#5807,#5808,#5809,#5810,#5811,#5812,#5813,#5814,#5815,#5816,#5817,#5818,
#5819,#5820,#5821,#5822,#5823,#5824,#5825,#5826,#5827,#5828,#5829,#5830,
#5831,#5832,#5833,#5834,#5835,#5836,#5837,#5838,#5839,#5840,#5841,#5842,
#5843,#5844,#5845,#5846,#5847,#5848,#5849,#5850,#5851,#5852,#5853,#5854,
#5855,#5856,#5857,#5858,#5859,#5860,#5861,#5862,#5863,#5864,#5865,#5866,
#5867,#5868,#5869,#5870,#5871,#5872,#5873,#5874,#5875,#5876),
 .UNSPECIFIED.,.F.,.F.,(4,3,3,3,3,3,3,3,3,3,3,3,3,3,3,3,3,3,3,3,3,3,3,3,
3,3,3,3,3,3,3,3,3,3,3,3,3,4),(17.9335665904152,18.0454424339238,18.1573652595226,
18.2695047672841,18.3736626818853,18.4855001980023,18.5971371009513,18.708662064031,
18.8201184282184,18.9315494357043,19.0430804470575,19.1546580302906,19.2664507586058,
19.3674783206137,19.4794788083052,19.5912816496511,19.7029742420256,19.8145996336116,
19.9262007760276,20.0379022986976,20.1496508775319,20.2616132084707,20.3612939593421,
20.4732878287697,20.5850846606291,20.6967716191335,20.8083917627454,20.9199880538123,
21.0316853912131,21.143430143744,21.2553893075683,21.3551095980704,21.467587143227,
21.5798851258176,21.6920363292369,21.8041004131203,21.9161448818857,21.9911485751285),
 .UNSPECIFIED.);
#78=B_SPLINE_CURVE_WITH_KNOTS('',3,(#5974,#5975,#5976,#5977,#5978,#5979,
#5980,#5981,#5982,#5983,#5984,#5985,#5986,#5987,#5988,#5989,#5990,#5991,
#5992,#5993,#5994,#5995,#5996,#5997,#5998,#5999,#6000,#6001,#6002,#6003,
#6004,#6005,#6006,#6007,#6008,#6009,#6010,#6011,#6012,#6013,#6014,#6015,
#6016,#6017,#6018,#6019,#6020,#6021,#6022,#6023,#6024,#6025,#6026,#6027,
#6028,#6029,#6030,#6031,#6032,#6033,#6034,#6035,#6036,#6037,#6038,#6039,
#6040,#6041,#6042,#6043,#6044,#6045,#6046,#6047,#6048,#6049,#6050,#6051,
#6052),.UNSPECIFIED.,.F.,.F.,(4,3,3,3,3,3,3,3,3,3,3,3,3,3,3,3,3,3,3,3,3,
3,3,3,3,3,4),(0.,0.0179048422970877,0.0361024915626215,0.0542404355784353,
0.0580134783300132,0.0611348681368874,0.0788899039747601,0.0963378629766525,
0.10916026369559,0.115724976061314,0.119100678912912,0.13593778804363,0.147800793130485,
0.16459229773457,0.169382843385744,0.173083715163794,0.189811925251359,
0.206538015292767,0.216907909431901,0.222250091057922,0.226942734525874,
0.243039503413473,0.25318826724009,0.25808162694784,0.273544260851943,0.28213282996317,
0.286347380332243),.UNSPECIFIED.);
#79=B_SPLINE_CURVE_WITH_KNOTS('',3,(#6053,#6054,#6055,#6056,#6057,#6058,
#6059,#6060,#6061,#6062,#6063,#6064,#6065,#6066,#6067,#6068,#6069,#6070,
#6071,#6072,#6073,#6074,#6075,#6076,#6077,#6078,#6079,#6080,#6081,#6082,
#6083,#6084,#6085,#6086,#6087,#6088,#6089,#6090,#6091,#6092,#6093,#6094,
#6095,#6096,#6097,#6098,#6099,#6100,#6101,#6102,#6103,#6104,#6105,#6106,
#6107,#6108,#6109,#6110,#6111,#6112,#6113,#6114,#6115,#6116,#6117,#6118,
#6119,#6120,#6121,#6122,#6123,#6124,#6125,#6126,#6127,#6128,#6129,#6130,
#6131,#6132,#6133,#6134),.UNSPECIFIED.,.F.,.F.,(4,3,3,3,3,3,3,3,3,3,3,3,
3,3,3,3,3,3,3,3,3,3,3,3,3,3,3,4),(1.07126707893266E-15,0.0152281422359197,
0.0310358564807719,0.0437698821708955,0.0495880457978997,0.0523050824654196,
0.0686461535426187,0.0852625440655788,0.0972830200437303,0.101409276797269,
0.104348930321076,0.121427316920974,0.133459759972985,0.150098458592417,
0.154673008198034,0.158573193033796,0.175469189003421,0.192923999237044,
0.203913467919425,0.209199575070649,0.212499609675233,0.215890121723282,
0.233888353561583,0.246488524940927,0.251400213167848,0.269588946346959,
0.280063647041007,0.285111243506067),.UNSPECIFIED.);
#80=B_SPLINE_CURVE_WITH_KNOTS('',3,(#6135,#6136,#6137,#6138),
 .UNSPECIFIED.,.F.,.F.,(4,4),(-0.0155829349012829,0.),.UNSPECIFIED.);
#81=B_SPLINE_CURVE_WITH_KNOTS('',3,(#6235,#6236,#6237,#6238,#6239,#6240,
#6241,#6242,#6243,#6244,#6245,#6246,#6247,#6248,#6249,#6250,#6251,#6252,
#6253,#6254,#6255,#6256,#6257,#6258,#6259,#6260,#6261,#6262,#6263,#6264,
#6265,#6266,#6267,#6268,#6269,#6270,#6271,#6272,#6273,#6274,#6275,#6276,
#6277,#6278,#6279,#6280,#6281,#6282,#6283,#6284,#6285,#6286,#6287,#6288,
#6289,#6290,#6291,#6292,#6293,#6294,#6295,#6296,#6297,#6298,#6299,#6300,
#6301,#6302,#6303,#6304,#6305,#6306,#6307,#6308,#6309,#6310,#6311,#6312,
#6313,#6314,#6315,#6316),.UNSPECIFIED.,.F.,.F.,(4,3,3,3,3,3,3,3,3,3,3,3,
3,3,3,3,3,3,3,3,3,3,3,3,3,3,3,4),(0.,0.0152282227773072,0.0310359955541488,
0.043770002841855,0.0495884887043898,0.053412115752948,0.0697756354439873,
0.0863907647498071,0.0972836205062952,0.101414423606461,0.104352797521847,
0.121431164597359,0.133459759972988,0.15009841762802,0.154672953836668,
0.158573187410825,0.175469130012791,0.192923920449733,0.203913403642419,
0.209199537217335,0.212499486961885,0.219647292536604,0.237645810922074,
0.246488478012031,0.251400187912865,0.269588921026693,0.280063647041022,
0.285128810487037),.UNSPECIFIED.);
#82=B_SPLINE_CURVE_WITH_KNOTS('',3,(#6317,#6318,#6319,#6320,#6321,#6322,
#6323,#6324,#6325,#6326,#6327,#6328,#6329,#6330,#6331,#6332,#6333,#6334,
#6335,#6336,#6337,#6338,#6339,#6340,#6341,#6342,#6343,#6344,#6345,#6346,
#6347,#6348,#6349,#6350,#6351,#6352,#6353,#6354,#6355,#6356,#6357,#6358,
#6359,#6360,#6361,#6362,#6363,#6364,#6365,#6366,#6367,#6368,#6369,#6370,
#6371,#6372,#6373,#6374,#6375,#6376,#6377,#6378,#6379,#6380,#6381,#6382,
#6383,#6384,#6385,#6386,#6387,#6388,#6389,#6390,#6391,#6392,#6393,#6394,
#6395),.UNSPECIFIED.,.F.,.F.,(4,3,3,3,3,3,3,3,3,3,3,3,3,3,3,3,3,3,3,3,3,
3,3,3,3,3,4),(0.,0.017904897346114,0.0361025664030719,0.0542404915517878,
0.0580134882355451,0.0611348756782414,0.0788871339356662,0.0973060528525341,
0.114370955860744,0.115724971769402,0.119100681284986,0.135937768656981,
0.147800793130486,0.164592297734572,0.169382837867022,0.173083711575593,
0.189811921998653,0.206538004930166,0.216907939748199,0.222250091872117,
0.226243992006493,0.242350705801912,0.25318821167206,0.258081617490871,
0.273544209260892,0.282132829963172,0.286347380332245),.UNSPECIFIED.);
#347=SHAPE_REPRESENTATION_RELATIONSHIP('SRR','None',#40768,#355);
#355=ADVANCED_BREP_SHAPE_REPRESENTATION('',(#372),#40728);
#363=STYLED_ITEM('',(#40815),#372);
#372=MANIFOLD_SOLID_BREP('Body1',#3168);
#385=FACE_BOUND('',#616,.T.);
#386=FACE_BOUND('',#624,.T.);
#400=PLANE('',#3312);
#401=PLANE('',#3313);
#402=PLANE('',#3314);
#403=PLANE('',#3315);
#404=PLANE('',#3316);
#405=PLANE('',#3317);
#406=PLANE('',#3318);
#407=PLANE('',#3319);
#441=FACE_OUTER_BOUND('',#605,.T.);
#442=FACE_OUTER_BOUND('',#606,.T.);
#443=FACE_OUTER_BOUND('',#607,.T.);
#444=FACE_OUTER_BOUND('',#608,.T.);
#445=FACE_OUTER_BOUND('',#609,.T.);
#446=FACE_OUTER_BOUND('',#610,.T.);
#447=FACE_OUTER_BOUND('',#611,.T.);
#448=FACE_OUTER_BOUND('',#612,.T.);
#449=FACE_OUTER_BOUND('',#613,.T.);
#450=FACE_OUTER_BOUND('',#614,.T.);
#451=FACE_OUTER_BOUND('',#615,.T.);
#452=FACE_OUTER_BOUND('',#617,.T.);
#453=FACE_OUTER_BOUND('',#618,.T.);
#454=FACE_OUTER_BOUND('',#619,.T.);
#455=FACE_OUTER_BOUND('',#620,.T.);
#456=FACE_OUTER_BOUND('',#621,.T.);
#457=FACE_OUTER_BOUND('',#622,.T.);
#458=FACE_OUTER_BOUND('',#623,.T.);
#605=EDGE_LOOP('',(#1968,#1969,#1970,#1971));
#606=EDGE_LOOP('',(#1972,#1973,#1974,#1975,#1976,#1977));
#607=EDGE_LOOP('',(#1978,#1979,#1980,#1981,#1982,#1983));
#608=EDGE_LOOP('',(#1984,#1985,#1986,#1987,#1988));
#609=EDGE_LOOP('',(#1989,#1990,#1991,#1992,#1993,#1994));
#610=EDGE_LOOP('',(#1995,#1996,#1997,#1998));
#611=EDGE_LOOP('',(#1999,#2000,#2001,#2002,#2003,#2004));
#612=EDGE_LOOP('',(#2005,#2006,#2007,#2008,#2009,#2010));
#613=EDGE_LOOP('',(#2011,#2012,#2013,#2014,#2015,#2016,#2017,#2018,#2019,
#2020,#2021,#2022,#2023,#2024,#2025,#2026));
#614=EDGE_LOOP('',(#2027,#2028,#2029,#2030,#2031,#2032,#2033,#2034,#2035,
#2036,#2037,#2038,#2039,#2040,#2041,#2042));
#615=EDGE_LOOP('',(#2043,#2044,#2045,#2046,#2047,#2048));
#616=EDGE_LOOP('',(#2049,#2050,#2051,#2052));
#617=EDGE_LOOP('',(#2053,#2054,#2055,#2056));
#618=EDGE_LOOP('',(#2057,#2058,#2059,#2060));
#619=EDGE_LOOP('',(#2061,#2062,#2063,#2064));
#620=EDGE_LOOP('',(#2065,#2066,#2067,#2068));
#621=EDGE_LOOP('',(#2069,#2070,#2071,#2072));
#622=EDGE_LOOP('',(#2073,#2074,#2075,#2076));
#623=EDGE_LOOP('',(#2077,#2078,#2079,#2080,#2081,#2082));
#624=EDGE_LOOP('',(#2083,#2084,#2085,#2086,#2087));
#762=LINE('',#4119,#904);
#763=LINE('',#4208,#905);
#764=LINE('',#4511,#906);
#765=LINE('',#4645,#907);
#766=LINE('',#4801,#908);
#767=LINE('',#5118,#909);
#768=LINE('',#6399,#910);
#769=LINE('',#6401,#911);
#770=LINE('',#6403,#912);
#771=LINE('',#6405,#913);
#772=LINE('',#6407,#914);
#773=LINE('',#6408,#915);
#774=LINE('',#6411,#916);
#775=LINE('',#6413,#917);
#776=LINE('',#6414,#918);
#777=LINE('',#6417,#919);
#778=LINE('',#6418,#920);
#779=LINE('',#6421,#921);
#780=LINE('',#6422,#922);
#781=LINE('',#6425,#923);
#782=LINE('',#6426,#924);
#783=LINE('',#6429,#925);
#784=LINE('',#6430,#926);
#785=LINE('',#6432,#927);
#904=VECTOR('',#3561,1.543);
#905=VECTOR('',#3566,1.543);
#906=VECTOR('',#3569,1.543);
#907=VECTOR('',#3574,1.2645);
#908=VECTOR('',#3579,1.2645);
#909=VECTOR('',#3582,1.2645);
#910=VECTOR('',#3591,10.);
#911=VECTOR('',#3592,9.99999999999999);
#912=VECTOR('',#3593,10.);
#913=VECTOR('',#3594,10.);
#914=VECTOR('',#3595,10.);
#915=VECTOR('',#3596,10.);
#916=VECTOR('',#3599,10.);
#917=VECTOR('',#3600,9.99999999999999);
#918=VECTOR('',#3601,10.);
#919=VECTOR('',#3604,10.);
#920=VECTOR('',#3605,10.);
#921=VECTOR('',#3608,10.);
#922=VECTOR('',#3609,10.);
#923=VECTOR('',#3612,10.);
#924=VECTOR('',#3613,10.);
#925=VECTOR('',#3616,10.);
#926=VECTOR('',#3617,10.);
#927=VECTOR('',#3620,10.);
#1059=CIRCLE('',#3301,1.543);
#1060=CIRCLE('',#3304,1.543);
#1061=CIRCLE('',#3306,1.2645);
#1062=CIRCLE('',#3309,1.2645);
#1105=VERTEX_POINT('',#4117);
#1106=VERTEX_POINT('',#4118);
#1107=VERTEX_POINT('',#4120);
#1108=VERTEX_POINT('',#4127);
#1109=VERTEX_POINT('',#4206);
#1110=VERTEX_POINT('',#4207);
#1111=VERTEX_POINT('',#4209);
#1112=VERTEX_POINT('',#4328);
#1113=VERTEX_POINT('',#4509);
#1114=VERTEX_POINT('',#4510);
#1115=VERTEX_POINT('',#4512);
#1116=VERTEX_POINT('',#4574);
#1117=VERTEX_POINT('',#4580);
#1118=VERTEX_POINT('',#4582);
#1119=VERTEX_POINT('',#4643);
#1120=VERTEX_POINT('',#4644);
#1121=VERTEX_POINT('',#4646);
#1122=VERTEX_POINT('',#4699);
#1123=VERTEX_POINT('',#4714);
#1124=VERTEX_POINT('',#4799);
#1125=VERTEX_POINT('',#4800);
#1126=VERTEX_POINT('',#4802);
#1127=VERTEX_POINT('',#4979);
#1128=VERTEX_POINT('',#5116);
#1129=VERTEX_POINT('',#5117);
#1130=VERTEX_POINT('',#5119);
#1131=VERTEX_POINT('',#5172);
#1132=VERTEX_POINT('',#5275);
#1133=VERTEX_POINT('',#5452);
#1134=VERTEX_POINT('',#5630);
#1135=VERTEX_POINT('',#5703);
#1136=VERTEX_POINT('',#5973);
#1137=VERTEX_POINT('',#6397);
#1138=VERTEX_POINT('',#6398);
#1139=VERTEX_POINT('',#6400);
#1140=VERTEX_POINT('',#6402);
#1141=VERTEX_POINT('',#6404);
#1142=VERTEX_POINT('',#6406);
#1143=VERTEX_POINT('',#6410);
#1144=VERTEX_POINT('',#6412);
#1145=VERTEX_POINT('',#6416);
#1146=VERTEX_POINT('',#6420);
#1147=VERTEX_POINT('',#6424);
#1148=VERTEX_POINT('',#6428);
#1460=EDGE_CURVE('',#1105,#1106,#762,.T.);
#1461=EDGE_CURVE('',#1106,#1107,#51,.T.);
#1462=EDGE_CURVE('',#1108,#1107,#1059,.T.);
#1463=EDGE_CURVE('',#1105,#1108,#52,.T.);
#1464=EDGE_CURVE('',#1109,#1110,#763,.T.);
#1465=EDGE_CURVE('',#1110,#1111,#53,.T.);
#1466=EDGE_CURVE('',#1111,#1106,#54,.T.);
#1467=EDGE_CURVE('',#1112,#1105,#55,.T.);
#1468=EDGE_CURVE('',#1109,#1112,#56,.T.);
#1469=EDGE_CURVE('',#1113,#1114,#764,.T.);
#1470=EDGE_CURVE('',#1115,#1113,#57,.T.);
#1471=EDGE_CURVE('',#1116,#1115,#58,.T.);
#1472=EDGE_CURVE('',#1117,#1116,#1060,.T.);
#1473=EDGE_CURVE('',#1117,#1118,#59,.T.);
#1474=EDGE_CURVE('',#1118,#1114,#60,.T.);
#1475=EDGE_CURVE('',#1119,#1120,#765,.T.);
#1476=EDGE_CURVE('',#1120,#1121,#61,.T.);
#1477=EDGE_CURVE('',#1121,#1122,#62,.T.);
#1478=EDGE_CURVE('',#1123,#1122,#1061,.T.);
#1479=EDGE_CURVE('',#1123,#1119,#63,.T.);
#1480=EDGE_CURVE('',#1124,#1125,#766,.T.);
#1481=EDGE_CURVE('',#1125,#1126,#64,.T.);
#1482=EDGE_CURVE('',#1126,#1120,#65,.T.);
#1483=EDGE_CURVE('',#1119,#1127,#66,.T.);
#1484=EDGE_CURVE('',#1127,#1124,#67,.T.);
#1485=EDGE_CURVE('',#1128,#1129,#767,.T.);
#1486=EDGE_CURVE('',#1128,#1130,#68,.T.);
#1487=EDGE_CURVE('',#1131,#1130,#1062,.F.);
#1488=EDGE_CURVE('',#1131,#1129,#69,.T.);
#1489=EDGE_CURVE('',#1129,#1132,#70,.T.);
#1490=EDGE_CURVE('',#1132,#1125,#71,.T.);
#1491=EDGE_CURVE('',#1124,#1133,#72,.T.);
#1492=EDGE_CURVE('',#1133,#1128,#73,.T.);
#1493=EDGE_CURVE('',#1114,#1134,#74,.T.);
#1494=EDGE_CURVE('',#1134,#1110,#75,.T.);
#1495=EDGE_CURVE('',#1135,#1109,#76,.T.);
#1496=EDGE_CURVE('',#1113,#1135,#77,.T.);
#1497=EDGE_CURVE('',#1107,#1136,#78,.T.);
#1498=EDGE_CURVE('',#1130,#1117,#79,.T.);
#1499=EDGE_CURVE('',#1136,#1123,#80,.T.);
#1500=EDGE_CURVE('',#1122,#1108,#81,.T.);
#1501=EDGE_CURVE('',#1116,#1131,#82,.T.);
#1502=EDGE_CURVE('',#1137,#1138,#768,.T.);
#1503=EDGE_CURVE('',#1138,#1139,#769,.T.);
#1504=EDGE_CURVE('',#1139,#1140,#770,.T.);
#1505=EDGE_CURVE('',#1140,#1141,#771,.T.);
#1506=EDGE_CURVE('',#1141,#1142,#772,.T.);
#1507=EDGE_CURVE('',#1142,#1137,#773,.T.);
#1508=EDGE_CURVE('',#1138,#1143,#774,.T.);
#1509=EDGE_CURVE('',#1144,#1143,#775,.T.);
#1510=EDGE_CURVE('',#1139,#1144,#776,.T.);
#1511=EDGE_CURVE('',#1145,#1144,#777,.T.);
#1512=EDGE_CURVE('',#1140,#1145,#778,.T.);
#1513=EDGE_CURVE('',#1146,#1145,#779,.T.);
#1514=EDGE_CURVE('',#1141,#1146,#780,.T.);
#1515=EDGE_CURVE('',#1147,#1146,#781,.T.);
#1516=EDGE_CURVE('',#1142,#1147,#782,.T.);
#1517=EDGE_CURVE('',#1148,#1147,#783,.T.);
#1518=EDGE_CURVE('',#1137,#1148,#784,.T.);
#1519=EDGE_CURVE('',#1143,#1148,#785,.T.);
#1968=ORIENTED_EDGE('',*,*,#1460,.T.);
#1969=ORIENTED_EDGE('',*,*,#1461,.T.);
#1970=ORIENTED_EDGE('',*,*,#1462,.F.);
#1971=ORIENTED_EDGE('',*,*,#1463,.F.);
#1972=ORIENTED_EDGE('',*,*,#1464,.T.);
#1973=ORIENTED_EDGE('',*,*,#1465,.T.);
#1974=ORIENTED_EDGE('',*,*,#1466,.T.);
#1975=ORIENTED_EDGE('',*,*,#1460,.F.);
#1976=ORIENTED_EDGE('',*,*,#1467,.F.);
#1977=ORIENTED_EDGE('',*,*,#1468,.F.);
#1978=ORIENTED_EDGE('',*,*,#1469,.F.);
#1979=ORIENTED_EDGE('',*,*,#1470,.F.);
#1980=ORIENTED_EDGE('',*,*,#1471,.F.);
#1981=ORIENTED_EDGE('',*,*,#1472,.F.);
#1982=ORIENTED_EDGE('',*,*,#1473,.T.);
#1983=ORIENTED_EDGE('',*,*,#1474,.T.);
#1984=ORIENTED_EDGE('',*,*,#1475,.T.);
#1985=ORIENTED_EDGE('',*,*,#1476,.T.);
#1986=ORIENTED_EDGE('',*,*,#1477,.T.);
#1987=ORIENTED_EDGE('',*,*,#1478,.F.);
#1988=ORIENTED_EDGE('',*,*,#1479,.T.);
#1989=ORIENTED_EDGE('',*,*,#1480,.T.);
#1990=ORIENTED_EDGE('',*,*,#1481,.T.);
#1991=ORIENTED_EDGE('',*,*,#1482,.T.);
#1992=ORIENTED_EDGE('',*,*,#1475,.F.);
#1993=ORIENTED_EDGE('',*,*,#1483,.T.);
#1994=ORIENTED_EDGE('',*,*,#1484,.T.);
#1995=ORIENTED_EDGE('',*,*,#1485,.F.);
#1996=ORIENTED_EDGE('',*,*,#1486,.T.);
#1997=ORIENTED_EDGE('',*,*,#1487,.F.);
#1998=ORIENTED_EDGE('',*,*,#1488,.T.);
#1999=ORIENTED_EDGE('',*,*,#1485,.T.);
#2000=ORIENTED_EDGE('',*,*,#1489,.T.);
#2001=ORIENTED_EDGE('',*,*,#1490,.T.);
#2002=ORIENTED_EDGE('',*,*,#1480,.F.);
#2003=ORIENTED_EDGE('',*,*,#1491,.T.);
#2004=ORIENTED_EDGE('',*,*,#1492,.T.);
#2005=ORIENTED_EDGE('',*,*,#1469,.T.);
#2006=ORIENTED_EDGE('',*,*,#1493,.T.);
#2007=ORIENTED_EDGE('',*,*,#1494,.T.);
#2008=ORIENTED_EDGE('',*,*,#1464,.F.);
#2009=ORIENTED_EDGE('',*,*,#1495,.F.);
#2010=ORIENTED_EDGE('',*,*,#1496,.F.);
#2011=ORIENTED_EDGE('',*,*,#1497,.F.);
#2012=ORIENTED_EDGE('',*,*,#1461,.F.);
#2013=ORIENTED_EDGE('',*,*,#1466,.F.);
#2014=ORIENTED_EDGE('',*,*,#1465,.F.);
#2015=ORIENTED_EDGE('',*,*,#1494,.F.);
#2016=ORIENTED_EDGE('',*,*,#1493,.F.);
#2017=ORIENTED_EDGE('',*,*,#1474,.F.);
#2018=ORIENTED_EDGE('',*,*,#1473,.F.);
#2019=ORIENTED_EDGE('',*,*,#1498,.F.);
#2020=ORIENTED_EDGE('',*,*,#1486,.F.);
#2021=ORIENTED_EDGE('',*,*,#1492,.F.);
#2022=ORIENTED_EDGE('',*,*,#1491,.F.);
#2023=ORIENTED_EDGE('',*,*,#1484,.F.);
#2024=ORIENTED_EDGE('',*,*,#1483,.F.);
#2025=ORIENTED_EDGE('',*,*,#1479,.F.);
#2026=ORIENTED_EDGE('',*,*,#1499,.F.);
#2027=ORIENTED_EDGE('',*,*,#1500,.F.);
#2028=ORIENTED_EDGE('',*,*,#1477,.F.);
#2029=ORIENTED_EDGE('',*,*,#1476,.F.);
#2030=ORIENTED_EDGE('',*,*,#1482,.F.);
#2031=ORIENTED_EDGE('',*,*,#1481,.F.);
#2032=ORIENTED_EDGE('',*,*,#1490,.F.);
#2033=ORIENTED_EDGE('',*,*,#1489,.F.);
#2034=ORIENTED_EDGE('',*,*,#1488,.F.);
#2035=ORIENTED_EDGE('',*,*,#1501,.F.);
#2036=ORIENTED_EDGE('',*,*,#1471,.T.);
#2037=ORIENTED_EDGE('',*,*,#1470,.T.);
#2038=ORIENTED_EDGE('',*,*,#1496,.T.);
#2039=ORIENTED_EDGE('',*,*,#1495,.T.);
#2040=ORIENTED_EDGE('',*,*,#1468,.T.);
#2041=ORIENTED_EDGE('',*,*,#1467,.T.);
#2042=ORIENTED_EDGE('',*,*,#1463,.T.);
#2043=ORIENTED_EDGE('',*,*,#1502,.T.);
#2044=ORIENTED_EDGE('',*,*,#1503,.T.);
#2045=ORIENTED_EDGE('',*,*,#1504,.T.);
#2046=ORIENTED_EDGE('',*,*,#1505,.T.);
#2047=ORIENTED_EDGE('',*,*,#1506,.T.);
#2048=ORIENTED_EDGE('',*,*,#1507,.T.);
#2049=ORIENTED_EDGE('',*,*,#1498,.T.);
#2050=ORIENTED_EDGE('',*,*,#1472,.T.);
#2051=ORIENTED_EDGE('',*,*,#1501,.T.);
#2052=ORIENTED_EDGE('',*,*,#1487,.T.);
#2053=ORIENTED_EDGE('',*,*,#1503,.F.);
#2054=ORIENTED_EDGE('',*,*,#1508,.T.);
#2055=ORIENTED_EDGE('',*,*,#1509,.F.);
#2056=ORIENTED_EDGE('',*,*,#1510,.F.);
#2057=ORIENTED_EDGE('',*,*,#1504,.F.);
#2058=ORIENTED_EDGE('',*,*,#1510,.T.);
#2059=ORIENTED_EDGE('',*,*,#1511,.F.);
#2060=ORIENTED_EDGE('',*,*,#1512,.F.);
#2061=ORIENTED_EDGE('',*,*,#1505,.F.);
#2062=ORIENTED_EDGE('',*,*,#1512,.T.);
#2063=ORIENTED_EDGE('',*,*,#1513,.F.);
#2064=ORIENTED_EDGE('',*,*,#1514,.F.);
#2065=ORIENTED_EDGE('',*,*,#1506,.F.);
#2066=ORIENTED_EDGE('',*,*,#1514,.T.);
#2067=ORIENTED_EDGE('',*,*,#1515,.F.);
#2068=ORIENTED_EDGE('',*,*,#1516,.F.);
#2069=ORIENTED_EDGE('',*,*,#1507,.F.);
#2070=ORIENTED_EDGE('',*,*,#1516,.T.);
#2071=ORIENTED_EDGE('',*,*,#1517,.F.);
#2072=ORIENTED_EDGE('',*,*,#1518,.F.);
#2073=ORIENTED_EDGE('',*,*,#1502,.F.);
#2074=ORIENTED_EDGE('',*,*,#1518,.T.);
#2075=ORIENTED_EDGE('',*,*,#1519,.F.);
#2076=ORIENTED_EDGE('',*,*,#1508,.F.);
#2077=ORIENTED_EDGE('',*,*,#1519,.T.);
#2078=ORIENTED_EDGE('',*,*,#1517,.T.);
#2079=ORIENTED_EDGE('',*,*,#1515,.T.);
#2080=ORIENTED_EDGE('',*,*,#1513,.T.);
#2081=ORIENTED_EDGE('',*,*,#1511,.T.);
#2082=ORIENTED_EDGE('',*,*,#1509,.T.);
#2083=ORIENTED_EDGE('',*,*,#1497,.T.);
#2084=ORIENTED_EDGE('',*,*,#1499,.T.);
#2085=ORIENTED_EDGE('',*,*,#1478,.T.);
#2086=ORIENTED_EDGE('',*,*,#1500,.T.);
#2087=ORIENTED_EDGE('',*,*,#1462,.T.);
#2897=CYLINDRICAL_SURFACE('',#3300,1.543);
#2898=CYLINDRICAL_SURFACE('',#3302,1.543);
#2899=CYLINDRICAL_SURFACE('',#3303,1.543);
#2900=CYLINDRICAL_SURFACE('',#3305,1.2645);
#2901=CYLINDRICAL_SURFACE('',#3307,1.2645);
#2902=CYLINDRICAL_SURFACE('',#3308,1.2645);
#2903=CYLINDRICAL_SURFACE('',#3310,1.2645);
#2904=CYLINDRICAL_SURFACE('',#3311,1.543);
#3020=ADVANCED_FACE('',(#441),#2897,.F.);
#3021=ADVANCED_FACE('',(#442),#2898,.F.);
#3022=ADVANCED_FACE('',(#443),#2899,.F.);
#3023=ADVANCED_FACE('',(#444),#2900,.F.);
#3024=ADVANCED_FACE('',(#445),#2901,.F.);
#3025=ADVANCED_FACE('',(#446),#2902,.F.);
#3026=ADVANCED_FACE('',(#447),#2903,.F.);
#3027=ADVANCED_FACE('',(#448),#2904,.F.);
#3028=ADVANCED_FACE('',(#449),#43,.F.);
#3029=ADVANCED_FACE('',(#450),#44,.F.);
#3030=ADVANCED_FACE('',(#451,#385),#400,.T.);
#3031=ADVANCED_FACE('',(#452),#401,.T.);
#3032=ADVANCED_FACE('',(#453),#402,.T.);
#3033=ADVANCED_FACE('',(#454),#403,.T.);
#3034=ADVANCED_FACE('',(#455),#404,.T.);
#3035=ADVANCED_FACE('',(#456),#405,.T.);
#3036=ADVANCED_FACE('',(#457),#406,.T.);
#3037=ADVANCED_FACE('',(#458,#386),#407,.F.);
#3168=CLOSED_SHELL('',(#3020,#3021,#3022,#3023,#3024,#3025,#3026,#3027,
#3028,#3029,#3030,#3031,#3032,#3033,#3034,#3035,#3036,#3037));
#3299=AXIS2_PLACEMENT_3D('',#4115,#3557,#3558);
#3300=AXIS2_PLACEMENT_3D('',#4116,#3559,#3560);
#3301=AXIS2_PLACEMENT_3D('',#4128,#3562,#3563);
#3302=AXIS2_PLACEMENT_3D('',#4205,#3564,#3565);
#3303=AXIS2_PLACEMENT_3D('',#4508,#3567,#3568);
#3304=AXIS2_PLACEMENT_3D('',#4581,#3570,#3571);
#3305=AXIS2_PLACEMENT_3D('',#4642,#3572,#3573);
#3306=AXIS2_PLACEMENT_3D('',#4715,#3575,#3576);
#3307=AXIS2_PLACEMENT_3D('',#4798,#3577,#3578);
#3308=AXIS2_PLACEMENT_3D('',#5115,#3580,#3581);
#3309=AXIS2_PLACEMENT_3D('',#5173,#3583,#3584);
#3310=AXIS2_PLACEMENT_3D('',#5274,#3585,#3586);
#3311=AXIS2_PLACEMENT_3D('',#5629,#3587,#3588);
#3312=AXIS2_PLACEMENT_3D('',#6396,#3589,#3590);
#3313=AXIS2_PLACEMENT_3D('',#6409,#3597,#3598);
#3314=AXIS2_PLACEMENT_3D('',#6415,#3602,#3603);
#3315=AXIS2_PLACEMENT_3D('',#6419,#3606,#3607);
#3316=AXIS2_PLACEMENT_3D('',#6423,#3610,#3611);
#3317=AXIS2_PLACEMENT_3D('',#6427,#3614,#3615);
#3318=AXIS2_PLACEMENT_3D('',#6431,#3618,#3619);
#3319=AXIS2_PLACEMENT_3D('',#6433,#3621,#3622);
#3557=DIRECTION('axis',(0.,0.,1.));
#3558=DIRECTION('refdir',(1.,0.,0.));
#3559=DIRECTION('center_axis',(0.,0.,1.));
#3560=DIRECTION('ref_axis',(-0.609175761423683,0.793035239881479,0.));
#3561=DIRECTION('',(0.,0.,1.));
#3562=DIRECTION('center_axis',(0.,0.,-1.));
#3563=DIRECTION('ref_axis',(1.,4.24024356072764E-16,0.));
#3564=DIRECTION('center_axis',(0.,0.,1.));
#3565=DIRECTION('ref_axis',(-0.609175761423683,0.793035239881479,0.));
#3566=DIRECTION('',(0.,0.,1.));
#3567=DIRECTION('center_axis',(0.,0.,1.));
#3568=DIRECTION('ref_axis',(-0.609175761423683,0.793035239881479,0.));
#3569=DIRECTION('',(0.,0.,1.));
#3570=DIRECTION('center_axis',(0.,0.,1.));
#3571=DIRECTION('ref_axis',(1.,4.24024356072764E-16,0.));
#3572=DIRECTION('center_axis',(0.,0.,1.));
#3573=DIRECTION('ref_axis',(-0.348605484123622,-0.937269553777853,0.));
#3574=DIRECTION('',(0.,0.,1.));
#3575=DIRECTION('center_axis',(0.,0.,-1.));
#3576=DIRECTION('ref_axis',(1.,0.,0.));
#3577=DIRECTION('center_axis',(0.,0.,1.));
#3578=DIRECTION('ref_axis',(-0.348605484123622,-0.937269553777853,0.));
#3579=DIRECTION('',(0.,0.,1.));
#3580=DIRECTION('center_axis',(0.,0.,1.));
#3581=DIRECTION('ref_axis',(-0.348605484123622,-0.937269553777853,0.));
#3582=DIRECTION('',(0.,0.,1.));
#3583=DIRECTION('center_axis',(0.,0.,-1.));
#3584=DIRECTION('ref_axis',(1.,0.,0.));
#3585=DIRECTION('center_axis',(0.,0.,1.));
#3586=DIRECTION('ref_axis',(-0.348605484123622,-0.937269553777853,0.));
#3587=DIRECTION('center_axis',(0.,0.,1.));
#3588=DIRECTION('ref_axis',(-0.609175761423683,0.793035239881479,0.));
#3589=DIRECTION('center_axis',(0.,0.,-1.));
#3590=DIRECTION('ref_axis',(1.,0.,0.));
#3591=DIRECTION('',(1.,6.00925839494863E-16,0.));
#3592=DIRECTION('',(0.5,-0.866025403784439,0.));
#3593=DIRECTION('',(-0.499999999999999,-0.866025403784439,0.));
#3594=DIRECTION('',(-1.,-7.21111007393836E-16,0.));
#3595=DIRECTION('',(-0.500000000000001,0.866025403784438,0.));
#3596=DIRECTION('',(0.499999999999999,0.866025403784439,0.));
#3597=DIRECTION('center_axis',(0.866025403784438,0.5,0.));
#3598=DIRECTION('ref_axis',(-0.5,0.866025403784438,0.));
#3599=DIRECTION('',(0.,0.,1.));
#3600=DIRECTION('',(-0.5,0.866025403784439,0.));
#3601=DIRECTION('',(0.,0.,1.));
#3602=DIRECTION('center_axis',(0.866025403784439,-0.5,0.));
#3603=DIRECTION('ref_axis',(0.5,0.866025403784439,0.));
#3604=DIRECTION('',(0.499999999999999,0.866025403784439,0.));
#3605=DIRECTION('',(0.,0.,1.));
#3606=DIRECTION('center_axis',(7.21111007393836E-16,-1.,0.));
#3607=DIRECTION('ref_axis',(1.,7.21111007393836E-16,0.));
#3608=DIRECTION('',(1.,7.21111007393836E-16,0.));
#3609=DIRECTION('',(0.,0.,1.));
#3610=DIRECTION('center_axis',(-0.866025403784438,-0.500000000000001,0.));
#3611=DIRECTION('ref_axis',(0.500000000000001,-0.866025403784438,0.));
#3612=DIRECTION('',(0.500000000000001,-0.866025403784438,0.));
#3613=DIRECTION('',(0.,0.,1.));
#3614=DIRECTION('center_axis',(-0.866025403784439,0.499999999999999,0.));
#3615=DIRECTION('ref_axis',(-0.499999999999999,-0.866025403784439,0.));
#3616=DIRECTION('',(-0.499999999999999,-0.866025403784439,0.));
#3617=DIRECTION('',(0.,0.,1.));
#3618=DIRECTION('center_axis',(-6.00925839494863E-16,1.,0.));
#3619=DIRECTION('ref_axis',(-1.,-6.00925839494863E-16,0.));
#3620=DIRECTION('',(-1.,-6.00925839494863E-16,0.));
#3621=DIRECTION('center_axis',(0.,0.,-1.));
#3622=DIRECTION('ref_axis',(1.,0.,0.));
#4115=CARTESIAN_POINT('',(0.,0.,0.));
#4116=CARTESIAN_POINT('Origin',(3.53951905042299,8.32667268468867E-16,-7.60421172358873));
#4117=CARTESIAN_POINT('',(4.47947725029973,-1.22365337513712,-5.21861712256713));
#4118=CARTESIAN_POINT('',(4.47963717506662,-1.22386353108345,-5.17715717872024));
#4119=CARTESIAN_POINT('',(4.47947725029973,-1.22365337513712,-7.60421172358873));
#4120=CARTESIAN_POINT('',(3.93803289228021,1.49064942821852,-5.));
#4121=CARTESIAN_POINT('Ctrl Pts',(4.4796371750665,-1.22386353108354,-5.17715717872025));
#4122=CARTESIAN_POINT('Ctrl Pts',(4.57769164024551,-1.15008922561236,-5.17082834295539));
#4123=CARTESIAN_POINT('Ctrl Pts',(5.037452302555,-0.710090958920894,-5.13813772861957));
#4124=CARTESIAN_POINT('Ctrl Pts',(5.26960331241849,0.567664116001651,-5.07908533571283));
#4125=CARTESIAN_POINT('Ctrl Pts',(4.43184313015523,1.35863299878938,-5.02636177857094));
#4126=CARTESIAN_POINT('Ctrl Pts',(3.93803289228021,1.49064942821852,-5.));
#4127=CARTESIAN_POINT('',(3.14100461111498,1.49064926849444,-5.00001191998211));
#4128=CARTESIAN_POINT('Origin',(3.53951905042299,8.32667268468867E-16,-5.));
#4129=CARTESIAN_POINT('Ctrl Pts',(4.47947725029973,-1.22365337513712,-5.21861712256713));
#4130=CARTESIAN_POINT('Ctrl Pts',(4.52496896162635,-1.18870858770246,-5.21565841989965));
#4131=CARTESIAN_POINT('Ctrl Pts',(4.56856576972649,-1.15118013128263,-5.21269971723217));
#4132=CARTESIAN_POINT('Ctrl Pts',(4.60996354210099,-1.11130445434014,-5.20974101456469));
#4133=CARTESIAN_POINT('Ctrl Pts',(4.65133326839928,-1.07145579228783,-5.2067843163529));
#4134=CARTESIAN_POINT('Ctrl Pts',(4.69050653598573,-1.02926342304973,-5.20382761814111));
#4135=CARTESIAN_POINT('Ctrl Pts',(4.72721349442131,-0.985002998825653,-5.20087091992933));
#4136=CARTESIAN_POINT('Ctrl Pts',(4.763909812257,-0.940755404797399,-5.19791507880415));
#4137=CARTESIAN_POINT('Ctrl Pts',(4.79814090596258,-0.894441347385724,-5.19495923767897));
#4138=CARTESIAN_POINT('Ctrl Pts',(4.82967642307994,-0.846370458947444,-5.1920033965538));
#4139=CARTESIAN_POINT('Ctrl Pts',(4.86208679747809,-0.79696598949994,-5.18896555458115));
#4140=CARTESIAN_POINT('Ctrl Pts',(4.89164943609571,-0.745706210110481,-5.18592771260849));
#4141=CARTESIAN_POINT('Ctrl Pts',(4.91816268873484,-0.692957948610356,-5.18288987063584));
#4142=CARTESIAN_POINT('Ctrl Pts',(4.9439922730574,-0.641569848974656,-5.17993036217948));
#4143=CARTESIAN_POINT('Ctrl Pts',(4.96692770978701,-0.5887696387494,-5.17697085372312));
#4144=CARTESIAN_POINT('Ctrl Pts',(4.986831041283,-0.534917751727157,-5.17401134526675));
#4145=CARTESIAN_POINT('Ctrl Pts',(5.00752458742015,-0.478927803064939,-5.17093433653596));
#4146=CARTESIAN_POINT('Ctrl Pts',(5.0249399808018,-0.421801497406585,-5.16785732780516));
#4147=CARTESIAN_POINT('Ctrl Pts',(5.03897984230443,-0.363959247183371,-5.16478031907437));
#4148=CARTESIAN_POINT('Ctrl Pts',(5.05301970380706,-0.306116996960155,-5.16170331034357));
#4149=CARTESIAN_POINT('Ctrl Pts',(5.06368399482257,-0.247559432113643,-5.15862630161278));
#4150=CARTESIAN_POINT('Ctrl Pts',(5.07093548192274,-0.188713309897771,-5.15554929288199));
#4151=CARTESIAN_POINT('Ctrl Pts',(5.07794803979793,-0.131806108372223,-5.1525736685019));
#4152=CARTESIAN_POINT('Ctrl Pts',(5.08179867841453,-0.0743909914451671,
-5.14959804412181));
#4153=CARTESIAN_POINT('Ctrl Pts',(5.08242705471315,-0.0168490444052572,
-5.14662241974172));
#4154=CARTESIAN_POINT('Ctrl Pts',(5.08305431454027,0.0405906646226169,-5.14365208232074));
#4155=CARTESIAN_POINT('Ctrl Pts',(5.08047067165934,0.0981562413468887,-5.14068174489977));
#4156=CARTESIAN_POINT('Ctrl Pts',(5.07466750694301,0.155461302079316,-5.13771140747879));
#4157=CARTESIAN_POINT('Ctrl Pts',(5.06887011499728,0.21270935788678,-5.13474402483807));
#4158=CARTESIAN_POINT('Ctrl Pts',(5.05985959973971,0.26969689719103,-5.13177664219734));
#4159=CARTESIAN_POINT('Ctrl Pts',(5.04767935517533,0.326039100675548,-5.12880925955662));
#4160=CARTESIAN_POINT('Ctrl Pts',(5.03550658389236,0.382346734973937,-5.12584369757601));
#4161=CARTESIAN_POINT('Ctrl Pts',(5.02016804863226,0.438009311985927,-5.1228781355954));
#4162=CARTESIAN_POINT('Ctrl Pts',(5.00175846772087,0.492650876889871,-5.1199125736148));
#4163=CARTESIAN_POINT('Ctrl Pts',(4.9833531648314,0.547279744176552,-5.11694770077205));
#4164=CARTESIAN_POINT('Ctrl Pts',(4.96187839901806,0.600887578659077,-5.1139828279293));
#4165=CARTESIAN_POINT('Ctrl Pts',(4.93747847740791,0.653114416089551,-5.11101795508655));
#4166=CARTESIAN_POINT('Ctrl Pts',(4.91305752876829,0.705386260846979,-5.10805052721639));
#4167=CARTESIAN_POINT('Ctrl Pts',(4.88570660610911,0.756274258325724,-5.10508309934622));
#4168=CARTESIAN_POINT('Ctrl Pts',(4.85561728494828,0.805440523613895,-5.10211567147606));
#4169=CARTESIAN_POINT('Ctrl Pts',(4.82551583682365,0.854626604487657,-5.09914704763706));
#4170=CARTESIAN_POINT('Ctrl Pts',(4.79267408416198,0.902089140669927,-5.09617842379807));
#4171=CARTESIAN_POINT('Ctrl Pts',(4.75732677699548,0.947519572937856,-5.09320979995907));
#4172=CARTESIAN_POINT('Ctrl Pts',(4.72191366575164,0.99303458046536,-5.09023564960141));
#4173=CARTESIAN_POINT('Ctrl Pts',(4.68398602059646,1.03650953100728,-5.08726149924375));
#4174=CARTESIAN_POINT('Ctrl Pts',(4.64381804905404,1.07767004301988,-5.08428734888609));
#4175=CARTESIAN_POINT('Ctrl Pts',(4.60859793147866,1.11376044083883,-5.08167955164711));
#4176=CARTESIAN_POINT('Ctrl Pts',(4.57165616602179,1.14807187402944,-5.07907175440814));
#4177=CARTESIAN_POINT('Ctrl Pts',(4.53319812916631,1.1804452077364,-5.07646395716916));
#4178=CARTESIAN_POINT('Ctrl Pts',(4.48959378809824,1.21715061445732,-5.07350719469395));
#4179=CARTESIAN_POINT('Ctrl Pts',(4.443859421242,1.25151535266286,-5.07055043221873));
#4180=CARTESIAN_POINT('Ctrl Pts',(4.39627754539696,1.28328246356363,-5.06759366974352));
#4181=CARTESIAN_POINT('Ctrl Pts',(4.34877801436647,1.31499459855583,-5.06464202421784));
#4182=CARTESIAN_POINT('Ctrl Pts',(4.2994377530913,1.34411773663457,-5.06169037869217));
#4183=CARTESIAN_POINT('Ctrl Pts',(4.24857211196857,1.37043524323948,-5.05873873316649));
#4184=CARTESIAN_POINT('Ctrl Pts',(4.19775517201174,1.39672755222125,-5.05578991368557));
#4185=CARTESIAN_POINT('Ctrl Pts',(4.14541621046131,1.42021930978951,-5.05284109420466));
#4186=CARTESIAN_POINT('Ctrl Pts',(4.09189772583826,1.44073828259905,-5.04989227472374));
#4187=CARTESIAN_POINT('Ctrl Pts',(4.03840939328758,1.46124569511204,-5.04694511659439));
#4188=CARTESIAN_POINT('Ctrl Pts',(3.9837433454879,1.47878345424846,-5.04399795846504));
#4189=CARTESIAN_POINT('Ctrl Pts',(3.92826264938041,1.49322718106443,-5.04105080033569));
#4190=CARTESIAN_POINT('Ctrl Pts',(3.87279134964832,1.50766846164796,-5.03810414134579));
#4191=CARTESIAN_POINT('Ctrl Pts',(3.81650618504884,1.51901661846979,-5.03515748235589));
#4192=CARTESIAN_POINT('Ctrl Pts',(3.75978377510704,1.52719758088463,-5.03221082336599));
#4193=CARTESIAN_POINT('Ctrl Pts',(3.70300925473477,1.53538605908509,-5.02926145730373));
#4194=CARTESIAN_POINT('Ctrl Pts',(3.64579720902174,1.54040145688831,-5.02631209124146));
#4195=CARTESIAN_POINT('Ctrl Pts',(3.58853130954693,1.54222138438538,-5.0233627251792));
#4196=CARTESIAN_POINT('Ctrl Pts',(3.53123779596041,1.54404218946723,-5.02041193690713));
#4197=CARTESIAN_POINT('Ctrl Pts',(3.4738909038836,1.54266446818855,-5.01746114863506));
#4198=CARTESIAN_POINT('Ctrl Pts',(3.41687297221943,1.53811798620954,-5.01451036036299));
#4199=CARTESIAN_POINT('Ctrl Pts',(3.3597517542207,1.53356326840989,-5.01155422682328));
#4200=CARTESIAN_POINT('Ctrl Pts',(3.30296120866352,1.5258284006299,-5.00859809328357));
#4201=CARTESIAN_POINT('Ctrl Pts',(3.24687598530104,1.51499473148788,-5.00564195974387));
#4202=CARTESIAN_POINT('Ctrl Pts',(3.21127068834397,1.50811705526926,-5.00376527982328));
#4203=CARTESIAN_POINT('Ctrl Pts',(3.17594943093811,1.49999151658249,-5.00188859990269));
#4204=CARTESIAN_POINT('Ctrl Pts',(3.14100461111498,1.49064926849444,-5.00001191998211));
#4205=CARTESIAN_POINT('Origin',(3.53951905042299,8.32667268468867E-16,-7.60421172358873));
#4206=CARTESIAN_POINT('',(4.47947725029973,-1.22365337513712,-5.718702116292));
#4207=CARTESIAN_POINT('',(4.47947725029973,-1.22365337513712,-5.6770722010002));
#4208=CARTESIAN_POINT('',(4.47947725029973,-1.22365337513712,-7.60421172358873));
#4209=CARTESIAN_POINT('',(1.99678610450128,-0.000229152999684354,-5.35421171051895));
#4210=CARTESIAN_POINT('Ctrl Pts',(4.47947725029973,-1.22365337513712,-5.6770722010002));
#4211=CARTESIAN_POINT('Ctrl Pts',(4.52512102745272,-1.18859177723691,-5.6741124623146));
#4212=CARTESIAN_POINT('Ctrl Pts',(4.5688116981735,-1.15096420156402,-5.671152723629));
#4213=CARTESIAN_POINT('Ctrl Pts',(4.61025595191897,-1.11102272153849,-5.6681929849434));
#4214=CARTESIAN_POINT('Ctrl Pts',(4.65173647123993,-1.07104629093168,-5.66523065635408));
#4215=CARTESIAN_POINT('Ctrl Pts',(4.69096626732107,-1.02875227044639,-5.66226832776476));
#4216=CARTESIAN_POINT('Ctrl Pts',(4.7276881578121,-0.984430379583121,-5.65930599917544));
#4217=CARTESIAN_POINT('Ctrl Pts',(4.76442431086838,-0.940091274359376,-5.65634252003521));
#4218=CARTESIAN_POINT('Ctrl Pts',(4.79865030417651,-0.893723147399871,-5.65337904089497));
#4219=CARTESIAN_POINT('Ctrl Pts',(4.83015066651991,-0.845647108155074,-5.65041556175474));
#4220=CARTESIAN_POINT('Ctrl Pts',(4.86171249899614,-0.797477252830152,-5.64744629965067));
#4221=CARTESIAN_POINT('Ctrl Pts',(4.89053780680758,-0.747593276385191,-5.64447703754659));
#4222=CARTESIAN_POINT('Ctrl Pts',(4.91645618892747,-0.696342671826952,-5.64150777544252));
#4223=CARTESIAN_POINT('Ctrl Pts',(4.94213395443559,-0.645567858803961,-5.63856607886255));
#4224=CARTESIAN_POINT('Ctrl Pts',(4.96495844566623,-0.593452185264546,-5.63562438228257));
#4225=CARTESIAN_POINT('Ctrl Pts',(4.98481162376582,-0.540350235902651,-5.6326826857026));
#4226=CARTESIAN_POINT('Ctrl Pts',(5.00485343793378,-0.486743735435651,-5.62971303843008));
#4227=CARTESIAN_POINT('Ctrl Pts',(5.02195056381987,-0.431908927050247,-5.62674339115755));
#4228=CARTESIAN_POINT('Ctrl Pts',(5.03595542839796,-0.376200965805698,-5.62377374388503));
#4229=CARTESIAN_POINT('Ctrl Pts',(5.04993555413197,-0.320591409694572,-5.62080934233556));
#4230=CARTESIAN_POINT('Ctrl Pts',(5.0608341342622,-0.264112263761363,-5.61784494078608));
#4231=CARTESIAN_POINT('Ctrl Pts',(5.06855262957362,-0.20713597908089,-5.6148805392366));
#4232=CARTESIAN_POINT('Ctrl Pts',(5.07626350804143,-0.150215920313976,-5.61191906304784));
#4233=CARTESIAN_POINT('Ctrl Pts',(5.08080044975292,-0.0928002090382206,
-5.60895758685909));
#4234=CARTESIAN_POINT('Ctrl Pts',(5.08211585109736,-0.0352719513098852,
-5.60599611067033));
#4235=CARTESIAN_POINT('Ctrl Pts',(5.08343046125446,0.02222170433362,-5.60303641574968));
#4236=CARTESIAN_POINT('Ctrl Pts',(5.08152736026662,0.0798272519015085,-5.60007672082902));
#4237=CARTESIAN_POINT('Ctrl Pts',(5.07641092133383,0.13715821932413,-5.59711702590837));
#4238=CARTESIAN_POINT('Ctrl Pts',(5.07129558832057,0.194476794644151,-5.59415797072649));
#4239=CARTESIAN_POINT('Ctrl Pts',(5.06296834276969,0.251520388464657,-5.59119891554461));
#4240=CARTESIAN_POINT('Ctrl Pts',(5.05148550847944,0.307906527557052,-5.58823986036274));
#4241=CARTESIAN_POINT('Ctrl Pts',(5.03999228093245,0.364343702448172,-5.58527812690306));
#4242=CARTESIAN_POINT('Ctrl Pts',(5.02533786080861,0.42012172111455,-5.58231639344338));
#4243=CARTESIAN_POINT('Ctrl Pts',(5.00762968441671,0.474868577981904,-5.5793546599837));
#4244=CARTESIAN_POINT('Ctrl Pts',(4.9899140057136,0.529638629104231,-5.57639167174512));
#4245=CARTESIAN_POINT('Ctrl Pts',(4.96914217909774,0.583376159735024,-5.57342868350654));
#4246=CARTESIAN_POINT('Ctrl Pts',(4.94547043890925,0.635727687940012,-5.57046569526795));
#4247=CARTESIAN_POINT('Ctrl Pts',(4.92175318439951,0.68817987390206,-5.56749701000847));
#4248=CARTESIAN_POINT('Ctrl Pts',(4.89512511611778,0.739240268107272,-5.56452832474899));
#4249=CARTESIAN_POINT('Ctrl Pts',(4.86578877829008,0.788579488031072,-5.56155963948951));
#4250=CARTESIAN_POINT('Ctrl Pts',(4.83956118434086,0.83269027764405,-5.5589055429896));
#4251=CARTESIAN_POINT('Ctrl Pts',(4.81116967362603,0.875425510514394,-5.55625144648969));
#4252=CARTESIAN_POINT('Ctrl Pts',(4.780786696453,0.916571672548917,-5.55359734998977));
#4253=CARTESIAN_POINT('Ctrl Pts',(4.7467782835908,0.962627582678985,-5.55062655456604));
#4254=CARTESIAN_POINT('Ctrl Pts',(4.71013248018302,1.00688382228577,-5.5476557591423));
#4255=CARTESIAN_POINT('Ctrl Pts',(4.67106669050714,1.04902284923637,-5.54468496371856));
#4256=CARTESIAN_POINT('Ctrl Pts',(4.63206995983055,1.09108738443712,-5.54171941995263));
#4257=CARTESIAN_POINT('Ctrl Pts',(4.59066208558193,1.13104175687353,-5.53875387618669));
#4258=CARTESIAN_POINT('Ctrl Pts',(4.54710170338979,1.16860010159181,-5.53578833242076));
#4259=CARTESIAN_POINT('Ctrl Pts',(4.50358435587312,1.20612134123674,-5.53282571840904));
#4260=CARTESIAN_POINT('Ctrl Pts',(4.45791910652903,1.24125090469248,-5.52986310439732));
#4261=CARTESIAN_POINT('Ctrl Pts',(4.41040129674942,1.27373981371136,-5.5269004903856));
#4262=CARTESIAN_POINT('Ctrl Pts',(4.36291215771501,1.30620911994893,-5.52393966392159));
#4263=CARTESIAN_POINT('Ctrl Pts',(4.31357310338658,1.33604063673605,-5.52097883745757));
#4264=CARTESIAN_POINT('Ctrl Pts',(4.262710643379,1.36302711633986,-5.51801801099355));
#4265=CARTESIAN_POINT('Ctrl Pts',(4.21185931345673,1.39000769057023,-5.51505783243864));
#4266=CARTESIAN_POINT('Ctrl Pts',(4.15948569983316,1.41414421965574,-5.51209765388373));
#4267=CARTESIAN_POINT('Ctrl Pts',(4.10594129811614,1.43527517825616,-5.50913747532882));
#4268=CARTESIAN_POINT('Ctrl Pts',(4.05234884212578,1.45642510117083,-5.50617464011467));
#4269=CARTESIAN_POINT('Ctrl Pts',(3.99758398388154,1.47456387091719,-5.50321180490052));
#4270=CARTESIAN_POINT('Ctrl Pts',(3.94201732753734,1.48957850982081,-5.50024896968638));
#4271=CARTESIAN_POINT('Ctrl Pts',(3.88642732768093,1.50459945636339,-5.49728488978729));
#4272=CARTESIAN_POINT('Ctrl Pts',(3.83003536888944,1.51649354672025,-5.49432080988821));
#4273=CARTESIAN_POINT('Ctrl Pts',(3.77322316025061,1.52519880312361,-5.49135672998913));
#4274=CARTESIAN_POINT('Ctrl Pts',(3.71630234984157,1.53392070042648,-5.48838698397828));
#4275=CARTESIAN_POINT('Ctrl Pts',(3.65896020465046,1.53944153217191,-5.48541723796742));
#4276=CARTESIAN_POINT('Ctrl Pts',(3.60158350752301,1.54175127798387,-5.48244749195657));
#4277=CARTESIAN_POINT('Ctrl Pts',(3.55047795868461,1.54380857359876,-5.47980233273003));
#4278=CARTESIAN_POINT('Ctrl Pts',(3.49934528115122,1.54331910966274,-5.47715717350348));
#4279=CARTESIAN_POINT('Ctrl Pts',(3.44845565257208,1.54031050686926,-5.47451201427694));
#4280=CARTESIAN_POINT('Ctrl Pts',(3.39129979441924,1.53693144360425,-5.47154114673938));
#4281=CARTESIAN_POINT('Ctrl Pts',(3.3342138916778,1.53035977644368,-5.46857027920183));
#4282=CARTESIAN_POINT('Ctrl Pts',(3.27758271527957,1.52060460223282,-5.46559941166427));
#4283=CARTESIAN_POINT('Ctrl Pts',(3.22105127320109,1.51086660805822,-5.46263377618213));
#4284=CARTESIAN_POINT('Ctrl Pts',(3.16497347722393,1.49795632296522,-5.45966814069998));
#4285=CARTESIAN_POINT('Ctrl Pts',(3.10973002638419,1.48193467967241,-5.45670250521784));
#4286=CARTESIAN_POINT('Ctrl Pts',(3.05454093042656,1.4659288003212,-5.45373978767012));
#4287=CARTESIAN_POINT('Ctrl Pts',(3.00018505098282,1.44681777278669,-5.4507770701224));
#4288=CARTESIAN_POINT('Ctrl Pts',(2.94703217859048,1.42471341213106,-5.44781435257468));
#4289=CARTESIAN_POINT('Ctrl Pts',(2.8939111695424,1.40262230228996,-5.44485341107565));
#4290=CARTESIAN_POINT('Ctrl Pts',(2.84199221804376,1.37754161619727,-5.44189246957662));
#4291=CARTESIAN_POINT('Ctrl Pts',(2.79162712720225,1.34963205029415,-5.43893152807759));
#4292=CARTESIAN_POINT('Ctrl Pts',(2.74127286679701,1.32172848602371,-5.43597122329513));
#4293=CARTESIAN_POINT('Ctrl Pts',(2.69247225908117,1.29099750223447,-5.43301091851268));
#4294=CARTESIAN_POINT('Ctrl Pts',(2.6455524033983,1.25764567108841,-5.43005061373022));
#4295=CARTESIAN_POINT('Ctrl Pts',(2.59859018328914,1.22426372622673,-5.42708763605775));
#4296=CARTESIAN_POINT('Ctrl Pts',(2.55351253468013,1.18825650726338,-5.42412465838528));
#4297=CARTESIAN_POINT('Ctrl Pts',(2.51061628248063,1.14987307739617,-5.42116168071281));
#4298=CARTESIAN_POINT('Ctrl Pts',(2.46770187824625,1.11147340514596,-5.41819744922279));
#4299=CARTESIAN_POINT('Ctrl Pts',(2.42697108034768,1.07069588606239,-5.41523321773276));
#4300=CARTESIAN_POINT('Ctrl Pts',(2.38868401791696,1.0278267013251,-5.41226898624274));
#4301=CARTESIAN_POINT('Ctrl Pts',(2.35032360023518,0.984875382320805,-5.40929907549891));
#4302=CARTESIAN_POINT('Ctrl Pts',(2.31441660015544,0.939824798144525,-5.40632916475507));
#4303=CARTESIAN_POINT('Ctrl Pts',(2.28118236144417,0.892993716198393,-5.40335925401124));
#4304=CARTESIAN_POINT('Ctrl Pts',(2.25159302035572,0.851298738037958,-5.40071506219553));
#4305=CARTESIAN_POINT('Ctrl Pts',(2.22412184802125,0.808193041144038,-5.39807087037983));
#4306=CARTESIAN_POINT('Ctrl Pts',(2.19889289039257,0.763917861449834,-5.39542667856413));
#4307=CARTESIAN_POINT('Ctrl Pts',(2.1694007361956,0.712161049065484,-5.39233567044945));
#4308=CARTESIAN_POINT('Ctrl Pts',(2.14285864125366,0.658604878470103,-5.38924466233477));
#4309=CARTESIAN_POINT('Ctrl Pts',(2.11947982028678,0.603603831063202,-5.38615365422009));
#4310=CARTESIAN_POINT('Ctrl Pts',(2.09616542177511,0.548754344015884,-5.38307116365777));
#4311=CARTESIAN_POINT('Ctrl Pts',(2.07599713401881,0.492468323152804,-5.37998867309545));
#4312=CARTESIAN_POINT('Ctrl Pts',(2.05914207527831,0.435124133393559,-5.37690618253314));
#4313=CARTESIAN_POINT('Ctrl Pts',(2.04231496635934,0.377875034366083,-5.37382880349624));
#4314=CARTESIAN_POINT('Ctrl Pts',(2.02879030435349,0.319571690885604,-5.37075142445933));
#4315=CARTESIAN_POINT('Ctrl Pts',(2.01868679289945,0.260611290000743,-5.36767404542243));
#4316=CARTESIAN_POINT('Ctrl Pts',(2.00860191294967,0.201759615766563,-5.3646023412641));
#4317=CARTESIAN_POINT('Ctrl Pts',(2.00192571204157,0.142253746948874,-5.36153063710577));
#4318=CARTESIAN_POINT('Ctrl Pts',(1.9987263078915,0.0825028760850183,-5.35845893294744));
#4319=CARTESIAN_POINT('Ctrl Pts',(1.99725171501102,0.054963933005107,-5.35704319649454));
#4320=CARTESIAN_POINT('Ctrl Pts',(1.99651497203302,0.027373102629171,-5.35562746004163));
#4321=CARTESIAN_POINT('Ctrl Pts',(1.99651906740702,-0.000228938216534968,
-5.35421172358873));
#4322=CARTESIAN_POINT('Ctrl Pts',(1.99901526745067,-0.000230945958973693,
-5.35421160141548));
#4323=CARTESIAN_POINT('Ctrl Pts',(1.99878308421294,-0.245946535663003,-5.34158818189409));
#4324=CARTESIAN_POINT('Ctrl Pts',(2.16986900897196,-1.00442940714747,-5.30260298380174));
#4325=CARTESIAN_POINT('Ctrl Pts',(3.24055550621135,-1.73347751710041,-5.24358484290335));
#4326=CARTESIAN_POINT('Ctrl Pts',(4.16926105443531,-1.45738459198171,-5.19719012152633));
#4327=CARTESIAN_POINT('Ctrl Pts',(4.4796371750665,-1.22386353108354,-5.17715717872025));
#4328=CARTESIAN_POINT('',(1.99651909233433,-0.00035963648524883,-5.39578827645238));
#4329=CARTESIAN_POINT('Ctrl Pts',(1.99651909233452,-0.0003596372777212,
-5.39578827641127));
#4330=CARTESIAN_POINT('Ctrl Pts',(1.99652355962509,-0.0195262520735117,
-5.39479395094767));
#4331=CARTESIAN_POINT('Ctrl Pts',(1.99688513508193,-0.0386883289920865,
-5.39379962548406));
#4332=CARTESIAN_POINT('Ctrl Pts',(1.99760339341755,-0.0578368972324017,
-5.39280530002046));
#4333=CARTESIAN_POINT('Ctrl Pts',(1.99974937102273,-0.115048065662224,-5.3898345023682));
#4334=CARTESIAN_POINT('Ctrl Pts',(2.00508825750452,-0.172258466379416,-5.38686370471594));
#4335=CARTESIAN_POINT('Ctrl Pts',(2.01361936247661,-0.229083265048165,-5.38389290706369));
#4336=CARTESIAN_POINT('Ctrl Pts',(2.02213538638427,-0.285807610322849,-5.38092736110988));
#4337=CARTESIAN_POINT('Ctrl Pts',(2.03383235103549,-0.342147195438881,-5.37796181515608));
#4338=CARTESIAN_POINT('Ctrl Pts',(2.04865765425814,-0.397720124491333,-5.37499626920227));
#4339=CARTESIAN_POINT('Ctrl Pts',(2.06346831097628,-0.453238150845048,-5.37203365302883));
#4340=CARTESIAN_POINT('Ctrl Pts',(2.08140104899805,-0.507990520864456,-5.36907103685538));
#4341=CARTESIAN_POINT('Ctrl Pts',(2.10235215788664,-0.561605130850327,-5.36610842068194));
#4342=CARTESIAN_POINT('Ctrl Pts',(2.12329062533932,-0.615187390965849,-5.36314759208559));
#4343=CARTESIAN_POINT('Ctrl Pts',(2.14724366403913,-0.667632767584206,-5.36018676348925));
#4344=CARTESIAN_POINT('Ctrl Pts',(2.17405830089212,-0.718586071038539,-5.35722593489291));
#4345=CARTESIAN_POINT('Ctrl Pts',(2.20086706968364,-0.769528223973896,-5.35426575423837));
#4346=CARTESIAN_POINT('Ctrl Pts',(2.23053595067948,-0.818978491176606,-5.35130557358383));
#4347=CARTESIAN_POINT('Ctrl Pts',(2.26286556636343,-0.866605378265437,-5.34834539292929));
#4348=CARTESIAN_POINT('Ctrl Pts',(2.29522419602285,-0.914275007753285,-5.34538255568243));
#4349=CARTESIAN_POINT('Ctrl Pts',(2.33024803934686,-0.960117554562589,-5.34241971843557));
#4350=CARTESIAN_POINT('Ctrl Pts',(2.36769457816158,-1.00383086534,-5.33945688118871));
#4351=CARTESIAN_POINT('Ctrl Pts',(2.40515684780633,-1.04756253954122,-5.33649279929039));
#4352=CARTESIAN_POINT('Ctrl Pts',(2.44504348135292,-1.08916281683413,-5.33352871739207));
#4353=CARTESIAN_POINT('Ctrl Pts',(2.48707405043502,-1.12836542042032,-5.33056463549375));
#4354=CARTESIAN_POINT('Ctrl Pts',(2.52918496361848,-1.16764296227228,-5.32759488756468));
#4355=CARTESIAN_POINT('Ctrl Pts',(2.57344760042178,-1.20451333669098,-5.32462513963562));
#4356=CARTESIAN_POINT('Ctrl Pts',(2.61954806545789,-1.2387503327234,-5.32165539170656));
#4357=CARTESIAN_POINT('Ctrl Pts',(2.66060956316622,-1.26924508658379,-5.31901024924025));
#4358=CARTESIAN_POINT('Ctrl Pts',(2.70312842199546,-1.29765114353574,-5.31636510677394));
#4359=CARTESIAN_POINT('Ctrl Pts',(2.74686587636044,-1.32383909356408,-5.31371996430764));
#4360=CARTESIAN_POINT('Ctrl Pts',(2.79598933941203,-1.35325193466999,-5.31074908819936));
#4361=CARTESIAN_POINT('Ctrl Pts',(2.8468538816937,-1.37998776674441,-5.30777821209108));
#4362=CARTESIAN_POINT('Ctrl Pts',(2.89913649611857,-1.40383730686378,-5.3048073359828));
#4363=CARTESIAN_POINT('Ctrl Pts',(2.95132703607727,-1.42764484576153,-5.30184169185909));
#4364=CARTESIAN_POINT('Ctrl Pts',(3.00493022098378,-1.44857596748968,-5.29887604773538));
#4365=CARTESIAN_POINT('Ctrl Pts',(3.05959720111394,-1.46646650781932,-5.29591040361166));
#4366=CARTESIAN_POINT('Ctrl Pts',(3.11421039439706,-1.48433944564459,-5.29294767738549));
#4367=CARTESIAN_POINT('Ctrl Pts',(3.16988481632705,-1.49917756835214,-5.28998495115932));
#4368=CARTESIAN_POINT('Ctrl Pts',(3.22625195985338,-1.51086489467657,-5.28702222493315));
#4369=CARTESIAN_POINT('Ctrl Pts',(3.28258531370008,-1.52254521495125,-5.284061274734));
#4370=CARTESIAN_POINT('Ctrl Pts',(3.33961005679031,-1.53107837754764,-5.28110032453484));
#4371=CARTESIAN_POINT('Ctrl Pts',(3.39694500041986,-1.53639891963829,-5.27813937433569));
#4372=CARTESIAN_POINT('Ctrl Pts',(3.45426761498812,-1.5417183176223,-5.27517906084662));
#4373=CARTESIAN_POINT('Ctrl Pts',(3.511899779116,-1.54382641869227,-5.27221874735755));
#4374=CARTESIAN_POINT('Ctrl Pts',(3.5694548646447,-1.54270957961208,-5.26925843386848));
#4375=CARTESIAN_POINT('Ctrl Pts',(3.62706191594448,-1.54159173215177,-5.26629544754916));
#4376=CARTESIAN_POINT('Ctrl Pts',(3.68459122742742,-1.53724313542495,-5.26333246122985));
#4377=CARTESIAN_POINT('Ctrl Pts',(3.74165724076404,-1.52970230829585,-5.26036947491054));
#4378=CARTESIAN_POINT('Ctrl Pts',(3.79874740179333,-1.52215829023811,-5.2574052347927));
#4379=CARTESIAN_POINT('Ctrl Pts',(3.85537336070937,-1.51141944510768,-5.25444099467487));
#4380=CARTESIAN_POINT('Ctrl Pts',(3.91115896138416,-1.49757563300849,-5.25147675455704));
#4381=CARTESIAN_POINT('Ctrl Pts',(3.96705144023782,-1.48370529791039,-5.24850683532879));
#4382=CARTESIAN_POINT('Ctrl Pts',(4.02209984393975,-1.46671826238209,-5.24553691610055));
#4383=CARTESIAN_POINT('Ctrl Pts',(4.07594335058692,-1.44675428812001,-5.24256699687231));
#4384=CARTESIAN_POINT('Ctrl Pts',(4.12388029109525,-1.4289803371628,-5.23992287411314));
#4385=CARTESIAN_POINT('Ctrl Pts',(4.17086221813424,-1.40884756517063,-5.23727875135398));
#4386=CARTESIAN_POINT('Ctrl Pts',(4.21665074612344,-1.38648536475429,-5.23463462859482));
#4387=CARTESIAN_POINT('Ctrl Pts',(4.26800422218038,-1.36140535510795,-5.23166915010562));
#4388=CARTESIAN_POINT('Ctrl Pts',(4.31807087215149,-1.33341541556237,-5.22870367161642));
#4389=CARTESIAN_POINT('Ctrl Pts',(4.36650003494377,-1.30267089137703,-5.22573819312721));
#4390=CARTESIAN_POINT('Ctrl Pts',(4.40526471622146,-1.27806171764032,-5.22336450294052));
#4391=CARTESIAN_POINT('Ctrl Pts',(4.4429804336582,-1.25168866909262,-5.22099081275382));
#4392=CARTESIAN_POINT('Ctrl Pts',(4.47947725029973,-1.22365337513712,-5.21861712256713));
#4393=CARTESIAN_POINT('Ctrl Pts',(4.47947725029973,-1.22365337513712,-5.718702116292));
#4394=CARTESIAN_POINT('Ctrl Pts',(4.5250506460368,-1.18864584123114,-5.71573178326587));
#4395=CARTESIAN_POINT('Ctrl Pts',(4.56859375641112,-1.15114421804424,-5.71276145023973));
#4396=CARTESIAN_POINT('Ctrl Pts',(4.60983854390703,-1.1114248431037,-5.7097911172136));
#4397=CARTESIAN_POINT('Ctrl Pts',(4.6128215099069,-1.10855220022742,-5.70957629243299));
#4398=CARTESIAN_POINT('Ctrl Pts',(4.61579247143402,-1.10566797149909,-5.70936146765238));
#4399=CARTESIAN_POINT('Ctrl Pts',(4.61875133531101,-1.10277226808412,-5.70914664287176));
#4400=CARTESIAN_POINT('Ctrl Pts',(4.65965884843631,-1.062737974389,-5.70617660170126));
#4401=CARTESIAN_POINT('Ctrl Pts',(4.69842089249096,-1.02034104388721,-5.70320656053075));
#4402=CARTESIAN_POINT('Ctrl Pts',(4.73475305844049,-0.975840492128923,-5.70023651936025));
#4403=CARTESIAN_POINT('Ctrl Pts',(4.77102103844435,-0.931418556933201,-5.69727172519047));
#4404=CARTESIAN_POINT('Ctrl Pts',(4.80486733375244,-0.884900777484445,-5.6943069310207));
#4405=CARTESIAN_POINT('Ctrl Pts',(4.83604459506597,-0.836582639126709,-5.69134213685092));
#4406=CARTESIAN_POINT('Ctrl Pts',(4.8671910827755,-0.788312193324169,-5.68838026908962));
#4407=CARTESIAN_POINT('Ctrl Pts',(4.89567347497013,-0.738245345429881,-5.68541840132832));
#4408=CARTESIAN_POINT('Ctrl Pts',(4.92128602087865,-0.686708846133332,-5.68245653356702));
#4409=CARTESIAN_POINT('Ctrl Pts',(4.94688314864507,-0.635203370580891,-5.67949644877951));
#4410=CARTESIAN_POINT('Ctrl Pts',(4.96961362320494,-0.582230463341924,-5.676536363992));
#4411=CARTESIAN_POINT('Ctrl Pts',(4.98931732760889,-0.528141984194405,-5.67357627920449));
#4412=CARTESIAN_POINT('Ctrl Pts',(5.00901675787319,-0.474065237952958,-5.67061683652038));
#4413=CARTESIAN_POINT('Ctrl Pts',(5.02569054325441,-0.418873889913193,-5.66765739383628));
#4414=CARTESIAN_POINT('Ctrl Pts',(5.03922730215849,-0.362938231213574,-5.66469795115218));
#4415=CARTESIAN_POINT('Ctrl Pts',(5.05277628077117,-0.306952079079415,-5.66173583696247));
#4416=CARTESIAN_POINT('Ctrl Pts',(5.06318245047086,-0.250220781394763,-5.65877372277277));
#4417=CARTESIAN_POINT('Ctrl Pts',(5.07038515182195,-0.193126848437895,-5.65581160858307));
#4418=CARTESIAN_POINT('Ctrl Pts',(5.07759089676128,-0.136008789751712,-5.65284824271632));
#4419=CARTESIAN_POINT('Ctrl Pts',(5.08159043747568,-0.0785283114140747,
-5.64988487684958));
#4420=CARTESIAN_POINT('Ctrl Pts',(5.08237516046643,-0.0210718699127709,
-5.64692151098283));
#4421=CARTESIAN_POINT('Ctrl Pts',(5.08316138940842,0.0364948354656624,-5.64395245816087));
#4422=CARTESIAN_POINT('Ctrl Pts',(5.08072049402758,0.09403688916843,-5.6409834053389));
#4423=CARTESIAN_POINT('Ctrl Pts',(5.07509602117283,0.151169993393991,-5.63801435251694));
#4424=CARTESIAN_POINT('Ctrl Pts',(5.0700740281433,0.202183138729789,-5.63536333739761));
#4425=CARTESIAN_POINT('Ctrl Pts',(5.06251474258129,0.252870072794343,-5.63271232227827));
#4426=CARTESIAN_POINT('Ctrl Pts',(5.05248338402327,0.302965221194532,-5.63006130715894));
#4427=CARTESIAN_POINT('Ctrl Pts',(5.04124398616276,0.359093142501999,-5.62709104012201));
#4428=CARTESIAN_POINT('Ctrl Pts',(5.02685363357415,0.414711515953188,-5.62412077308509));
#4429=CARTESIAN_POINT('Ctrl Pts',(5.00937431062045,0.469440639559313,-5.62115050604816));
#4430=CARTESIAN_POINT('Ctrl Pts',(4.99192585970976,0.524073100390679,-5.61818548510755));
#4431=CARTESIAN_POINT('Ctrl Pts',(4.97139942469621,0.57781893626908,-5.61522046416694));
#4432=CARTESIAN_POINT('Ctrl Pts',(4.94790777060758,0.63030961666217,-5.61225544322633));
#4433=CARTESIAN_POINT('Ctrl Pts',(4.92443929913074,0.682748496911197,-5.6092933483006));
#4434=CARTESIAN_POINT('Ctrl Pts',(4.89801161826705,0.733934202401455,-5.60633125337487));
#4435=CARTESIAN_POINT('Ctrl Pts',(4.86878638733919,0.783516015795281,-5.60336915844913));
#4436=CARTESIAN_POINT('Ctrl Pts',(4.83957874786955,0.833067984552437,-5.60040884648858));
#4437=CARTESIAN_POINT('Ctrl Pts',(4.80757716062695,0.881017526855358,-5.59744853452803));
#4438=CARTESIAN_POINT('Ctrl Pts',(4.7729892208029,0.9270384775094,-5.59448822256748));
#4439=CARTESIAN_POINT('Ctrl Pts',(4.73840878763058,0.973049440195079,-5.5915285530861));
#4440=CARTESIAN_POINT('Ctrl Pts',(4.70124342942734,1.0171322258076,-5.58856888360472));
#4441=CARTESIAN_POINT('Ctrl Pts',(4.66174277275769,1.05899146220791,-5.58560921412333));
#4442=CARTESIAN_POINT('Ctrl Pts',(4.62220649312785,1.10088844861133,-5.58264687551701));
#4443=CARTESIAN_POINT('Ctrl Pts',(4.5803310645842,1.14055749815937,-5.57968453691068));
#4444=CARTESIAN_POINT('Ctrl Pts',(4.53640402249908,1.17773908504764,-5.57672219830435));
#4445=CARTESIAN_POINT('Ctrl Pts',(4.49245843394368,1.21493637040236,-5.57375860896676));
#4446=CARTESIAN_POINT('Ctrl Pts',(4.44645992134105,1.24964378394846,-5.57079501962917));
#4447=CARTESIAN_POINT('Ctrl Pts',(4.39872771866148,1.28164326722526,-5.56783143029157));
#4448=CARTESIAN_POINT('Ctrl Pts',(4.35090399238202,1.31370410756794,-5.5648621584514));
#4449=CARTESIAN_POINT('Ctrl Pts',(4.30134038312763,1.34304637521189,-5.56189288661123));
#4450=CARTESIAN_POINT('Ctrl Pts',(4.25038276935214,1.36949690511159,-5.55892361477106));
#4451=CARTESIAN_POINT('Ctrl Pts',(4.20491786967552,1.3930963360736,-5.55627440032941));
#4452=CARTESIAN_POINT('Ctrl Pts',(4.15834386516771,1.41439438923619,-5.55362518588776));
#4453=CARTESIAN_POINT('Ctrl Pts',(4.11091835799445,1.43330102606077,-5.55097597144611));
#4454=CARTESIAN_POINT('Ctrl Pts',(4.05774453158703,1.45449928590827,-5.54800565278781));
#4455=CARTESIAN_POINT('Ctrl Pts',(4.00327892648833,1.47277857230596,-5.5450353341295));
#4456=CARTESIAN_POINT('Ctrl Pts',(3.94787360955783,1.48798372102446,-5.5420650154712));
#4457=CARTESIAN_POINT('Ctrl Pts',(3.89256610051544,1.50316202785184,-5.53909994036371));
#4458=CARTESIAN_POINT('Ctrl Pts',(3.83632267091484,1.51527683172048,-5.53613486525623));
#4459=CARTESIAN_POINT('Ctrl Pts',(3.77951372278401,1.52422162339941,-5.53316979014875));
#4460=CARTESIAN_POINT('Ctrl Pts',(3.72276080637997,1.53315759266321,-5.53020763955023));
#4461=CARTESIAN_POINT('Ctrl Pts',(3.66544398895872,1.53892966400306,-5.52724548895171));
#4462=CARTESIAN_POINT('Ctrl Pts',(3.60794541203941,1.54148202488253,-5.5242833383532));
#4463=CARTESIAN_POINT('Ctrl Pts',(3.55048141736608,1.54403285065667,-5.52132296932609));
#4464=CARTESIAN_POINT('Ctrl Pts',(3.49283639960112,1.54336778169137,-5.51836260029899));
#4465=CARTESIAN_POINT('Ctrl Pts',(3.43539697819457,1.53948289827294,-5.51540223127188));
#4466=CARTESIAN_POINT('Ctrl Pts',(3.37796999777386,1.5355988562937,-5.51244250344046));
#4467=CARTESIAN_POINT('Ctrl Pts',(3.32074904510053,1.5284964197212,-5.50948277560903));
#4468=CARTESIAN_POINT('Ctrl Pts',(3.26411785739403,1.51822369329365,-5.50652304777761));
#4469=CARTESIAN_POINT('Ctrl Pts',(3.20743556993601,1.50794169752551,-5.50356064930899));
#4470=CARTESIAN_POINT('Ctrl Pts',(3.15134462507232,1.49448378804402,-5.50059825084036));
#4471=CARTESIAN_POINT('Ctrl Pts',(3.09621939422068,1.47794939521315,-5.49763585237174));
#4472=CARTESIAN_POINT('Ctrl Pts',(3.0410708721494,1.46140801635847,-5.49467220224625));
#4473=CARTESIAN_POINT('Ctrl Pts',(2.9868893689835,1.44178773967977,-5.49170855212077));
#4474=CARTESIAN_POINT('Ctrl Pts',(2.93403179183757,1.41923718232391,-5.48874490199529));
#4475=CARTESIAN_POINT('Ctrl Pts',(2.8810728522954,1.39664338086469,-5.48577556862258));
#4476=CARTESIAN_POINT('Ctrl Pts',(2.82944338102946,1.37110830140213,-5.48280623524988));
#4477=CARTESIAN_POINT('Ctrl Pts',(2.77947719277766,1.34282738080032,-5.47983690187717));
#4478=CARTESIAN_POINT('Ctrl Pts',(2.73490550162595,1.31759975182454,-5.47718814649588));
#4479=CARTESIAN_POINT('Ctrl Pts',(2.69165718122887,1.29018796291122,-5.47453939111459));
#4480=CARTESIAN_POINT('Ctrl Pts',(2.64994809620117,1.26075870705099,-5.47189063573329));
#4481=CARTESIAN_POINT('Ctrl Pts',(2.60346496462164,1.22796096115151,-5.46893870224377));
#4482=CARTESIAN_POINT('Ctrl Pts',(2.55869546569534,1.19251654365165,-5.46598676875425));
#4483=CARTESIAN_POINT('Ctrl Pts',(2.51595948046345,1.15463189231211,-5.46303483526472));
#4484=CARTESIAN_POINT('Ctrl Pts',(2.47329895141399,1.11681413146655,-5.46008811381444));
#4485=CARTESIAN_POINT('Ctrl Pts',(2.43266520432176,1.07656503309214,-5.45714139236415));
#4486=CARTESIAN_POINT('Ctrl Pts',(2.39434758436882,1.0341331216702,-5.45419467091387));
#4487=CARTESIAN_POINT('Ctrl Pts',(2.35606741861139,0.991742686026445,-5.45125082978552));
#4488=CARTESIAN_POINT('Ctrl Pts',(2.32009924872405,0.947174053247093,-5.44830698865717));
#4489=CARTESIAN_POINT('Ctrl Pts',(2.28669647218713,0.90071337697541,-5.44536314752882));
#4490=CARTESIAN_POINT('Ctrl Pts',(2.25331307243261,0.854279652307993,-5.44242101410788));
#4491=CARTESIAN_POINT('Ctrl Pts',(2.22249242482938,0.805956487503688,-5.43947888068694));
#4492=CARTESIAN_POINT('Ctrl Pts',(2.19444693579754,0.756062171026311,-5.436536747266));
#4493=CARTESIAN_POINT('Ctrl Pts',(2.16640657201678,0.706176972624892,-5.43359515151344));
#4494=CARTESIAN_POINT('Ctrl Pts',(2.14114061823626,0.654721653414925,-5.43065355576087));
#4495=CARTESIAN_POINT('Ctrl Pts',(2.11881630704433,0.602040459567581,-5.4277119600083));
#4496=CARTESIAN_POINT('Ctrl Pts',(2.09647190485982,0.549311854740122,-5.4247677169365));
#4497=CARTESIAN_POINT('Ctrl Pts',(2.07707463860601,0.49535565974548,-5.4218234738647));
#4498=CARTESIAN_POINT('Ctrl Pts',(2.06074356441428,0.440536107464182,-5.41887923079291));
#4499=CARTESIAN_POINT('Ctrl Pts',(2.0444047076198,0.385690430826799,-5.41593358463678));
#4500=CARTESIAN_POINT('Ctrl Pts',(2.03113507514356,0.329981092328246,-5.41298793848066));
#4501=CARTESIAN_POINT('Ctrl Pts',(2.02100294881358,0.273784311371141,-5.41004229232454));
#4502=CARTESIAN_POINT('Ctrl Pts',(2.01085268402028,0.217486927320778,-5.40709137289279));
#4503=CARTESIAN_POINT('Ctrl Pts',(2.00385120279259,0.160700883809956,-5.40414045346105));
#4504=CARTESIAN_POINT('Ctrl Pts',(2.00001494507583,0.103808042170368,-5.40118953402931));
#4505=CARTESIAN_POINT('Ctrl Pts',(1.9976743620204,0.0690965001028133,-5.399389114837));
#4506=CARTESIAN_POINT('Ctrl Pts',(1.99651100345573,0.034345238722842,-5.39758869564469));
#4507=CARTESIAN_POINT('Ctrl Pts',(1.99651909233433,-0.000359636485246585,
-5.39578827645238));
#4508=CARTESIAN_POINT('Origin',(3.53951905042299,8.32667268468867E-16,-7.60421172358873));
#4509=CARTESIAN_POINT('',(4.47947725029973,-1.22365337513712,-6.21868039134515));
#4510=CARTESIAN_POINT('',(4.48050266131609,-1.22496740309806,-6.17703688246106));
#4511=CARTESIAN_POINT('',(4.47947725029973,-1.22365337513712,-7.60421172358873));
#4512=CARTESIAN_POINT('',(1.99673565886186,0.00179124603277963,-6.39578836743343));
#4513=CARTESIAN_POINT('Ctrl Pts',(1.99652008837714,0.0017897277490038,-6.39578827641128));
#4514=CARTESIAN_POINT('Ctrl Pts',(1.99645403628334,-0.055156538086158,-6.39286004236045));
#4515=CARTESIAN_POINT('Ctrl Pts',(1.99954477721908,-0.11215736321612,-6.38993180830962));
#4516=CARTESIAN_POINT('Ctrl Pts',(2.00578359056079,-0.168832873461531,-6.38700357425878));
#4517=CARTESIAN_POINT('Ctrl Pts',(2.01202038127157,-0.22549000943717,-6.38407628954501));
#4518=CARTESIAN_POINT('Ctrl Pts',(2.02140316267154,-0.281821510112156,-6.38114900483125));
#4519=CARTESIAN_POINT('Ctrl Pts',(2.03387131239083,-0.33745205431088,-6.37822172011748));
#4520=CARTESIAN_POINT('Ctrl Pts',(2.04678845321045,-0.395085912538913,-6.37518902082222));
#4521=CARTESIAN_POINT('Ctrl Pts',(2.06301736691178,-0.451966755193889,-6.37215632152696));
#4522=CARTESIAN_POINT('Ctrl Pts',(2.08243330891811,-0.507690990567261,-6.36912362223169));
#4523=CARTESIAN_POINT('Ctrl Pts',(2.10119790125384,-0.561545836222492,-6.3661926613783));
#4524=CARTESIAN_POINT('Ctrl Pts',(2.12293876895841,-0.614319974748326,-6.3632617005249));
#4525=CARTESIAN_POINT('Ctrl Pts',(2.14749415252614,-0.665669350079501,-6.3603307396715));
#4526=CARTESIAN_POINT('Ctrl Pts',(2.17332807234279,-0.719692356532698,-6.35724717115531));
#4527=CARTESIAN_POINT('Ctrl Pts',(2.20227731628823,-0.772137569091362,-6.35416360263912));
#4528=CARTESIAN_POINT('Ctrl Pts',(2.23410044380417,-0.822636773730281,-6.35108003412292));
#4529=CARTESIAN_POINT('Ctrl Pts',(2.2659235713201,-0.873135978369199,-6.34799646560673));
#4530=CARTESIAN_POINT('Ctrl Pts',(2.30062011630072,-0.921688676698492,-6.34491289709054));
#4531=CARTESIAN_POINT('Ctrl Pts',(2.33790045788765,-0.967967849710609,-6.34182932857435));
#4532=CARTESIAN_POINT('Ctrl Pts',(2.3738540446845,-1.01260001221099,-6.33885549991368));
#4533=CARTESIAN_POINT('Ctrl Pts',(2.41237149952583,-1.05531795719075,-6.33588167125301));
#4534=CARTESIAN_POINT('Ctrl Pts',(2.45322151678262,-1.09581324522331,-6.33290784259233));
#4535=CARTESIAN_POINT('Ctrl Pts',(2.49399924564804,-1.13623687259509,-6.32993927643348));
#4536=CARTESIAN_POINT('Ctrl Pts',(2.53710097697729,-1.17444528766237,-6.32697071027463));
#4537=CARTESIAN_POINT('Ctrl Pts',(2.58225558169485,-1.21016348128613,-6.32400214411577));
#4538=CARTESIAN_POINT('Ctrl Pts',(2.62736548428903,-1.24584631463803,-6.32103651677592));
#4539=CARTESIAN_POINT('Ctrl Pts',(2.67452382749928,-1.27904349068993,-6.31807088943608));
#4540=CARTESIAN_POINT('Ctrl Pts',(2.7234243909379,-1.30951842551371,-6.31510526209623));
#4541=CARTESIAN_POINT('Ctrl Pts',(2.77229523555306,-1.3399748395037,-6.31214143708644));
#4542=CARTESIAN_POINT('Ctrl Pts',(2.82290576097275,-1.3677120178566,-6.30917761207666));
#4543=CARTESIAN_POINT('Ctrl Pts',(2.87492038146038,-1.39253639421493,-6.30621378706687));
#4544=CARTESIAN_POINT('Ctrl Pts',(2.92692327130035,-1.41735517203175,-6.30325063047659));
#4545=CARTESIAN_POINT('Ctrl Pts',(2.98032915856549,-1.43926222845626,-6.30028747388631));
#4546=CARTESIAN_POINT('Ctrl Pts',(3.03477942309202,-1.45811073262691,-6.29732431729602));
#4547=CARTESIAN_POINT('Ctrl Pts',(3.08927744992821,-1.47697577019921,-6.29435856150436));
#4548=CARTESIAN_POINT('Ctrl Pts',(3.14482119268528,-1.49277672287494,-6.2913928057127));
#4549=CARTESIAN_POINT('Ctrl Pts',(3.20103498306298,-1.50541606745226,-6.28842704992104));
#4550=CARTESIAN_POINT('Ctrl Pts',(3.25727185362023,-1.51806060147403,-6.28546007645351));
#4551=CARTESIAN_POINT('Ctrl Pts',(3.31417880676457,-1.52754085216985,-6.28249310298597));
#4552=CARTESIAN_POINT('Ctrl Pts',(3.37137119544686,-1.53381071155046,-6.27952612951844));
#4553=CARTESIAN_POINT('Ctrl Pts',(3.42867118730259,-1.54009236719945,-6.2765535739137));
#4554=CARTESIAN_POINT('Ctrl Pts',(3.48625716706642,-1.54315153299832,-6.27358101830897));
#4555=CARTESIAN_POINT('Ctrl Pts',(3.54374157597108,-1.5429942223735,-6.27060846270423));
#4556=CARTESIAN_POINT('Ctrl Pts',(3.59443694390479,-1.54285549049546,-6.26798697275666));
#4557=CARTESIAN_POINT('Ctrl Pts',(3.64505308062308,-1.54021596828826,-6.26536548280909));
#4558=CARTESIAN_POINT('Ctrl Pts',(3.69532853995772,-1.53511315640604,-6.26274399286153));
#4559=CARTESIAN_POINT('Ctrl Pts',(3.75238143557914,-1.5293224545896,-6.25976911019848));
#4560=CARTESIAN_POINT('Ctrl Pts',(3.80922524850646,-1.52033529212181,-6.25679422753544));
#4561=CARTESIAN_POINT('Ctrl Pts',(3.86547505287269,-1.50817826680635,-6.25381934487239));
#4562=CARTESIAN_POINT('Ctrl Pts',(3.92163253419786,-1.49604119486779,-6.2508493448968));
#4563=CARTESIAN_POINT('Ctrl Pts',(3.97719743813669,-1.48074469342844,-6.24787934492122));
#4564=CARTESIAN_POINT('Ctrl Pts',(4.03179118627241,-1.46236696634813,-6.24490934494563));
#4565=CARTESIAN_POINT('Ctrl Pts',(4.08633139370007,-1.44400726251324,-6.24194225768271));
#4566=CARTESIAN_POINT('Ctrl Pts',(4.13990184334824,-1.42257248758474,-6.23897517041978));
#4567=CARTESIAN_POINT('Ctrl Pts',(4.19213719523688,-1.39819117328771,-6.23600808315686));
#4568=CARTESIAN_POINT('Ctrl Pts',(4.24435372260801,-1.37381864550137,-6.23304206516952));
#4569=CARTESIAN_POINT('Ctrl Pts',(4.29523563084465,-1.34650189102749,-6.23007604718218));
#4570=CARTESIAN_POINT('Ctrl Pts',(4.34443752800149,-1.31641757981756,-6.22711002919483));
#4571=CARTESIAN_POINT('Ctrl Pts',(4.39104931259161,-1.28791698299728,-6.22430014991161));
#4572=CARTESIAN_POINT('Ctrl Pts',(4.43615314090438,-1.25693310345394,-6.22149027062838));
#4573=CARTESIAN_POINT('Ctrl Pts',(4.47947725029973,-1.22365337513712,-6.21868039134515));
#4574=CARTESIAN_POINT('',(3.14100520856574,1.49064942821851,-6.5));
#4575=CARTESIAN_POINT('Ctrl Pts',(3.14100520856575,1.49064942821851,-6.5));
#4576=CARTESIAN_POINT('Ctrl Pts',(2.64719497069073,1.35863299878936,-6.47363822142906));
#4577=CARTESIAN_POINT('Ctrl Pts',(2.09523405725447,0.837507597441754,-6.43890120269724));
#4578=CARTESIAN_POINT('Ctrl Pts',(1.99690773965972,0.164511449214008,-6.40416418396542));
#4579=CARTESIAN_POINT('Ctrl Pts',(1.99810069593897,0.00180086012095238,
-6.39578894380455));
#4580=CARTESIAN_POINT('',(3.93825622282343,1.49058970456196,-6.49999997840053));
#4581=CARTESIAN_POINT('Origin',(3.53951905042299,8.32667268468867E-16,-6.5));
#4582=CARTESIAN_POINT('',(1.99642704442048,-0.000970003776170875,-6.35421172358872));
#4583=CARTESIAN_POINT('Ctrl Pts',(3.93825622282343,1.49058970456196,-6.49999997840053));
#4584=CARTESIAN_POINT('Ctrl Pts',(3.88320017949414,1.50531735964604,-6.49704310510064));
#4585=CARTESIAN_POINT('Ctrl Pts',(3.82720821675325,1.51702233478024,-6.49408623180075));
#4586=CARTESIAN_POINT('Ctrl Pts',(3.77064508224469,1.52559160898792,-6.49112935850085));
#4587=CARTESIAN_POINT('Ctrl Pts',(3.71418095414078,1.53414588379649,-6.4881776608228));
#4588=CARTESIAN_POINT('Ctrl Pts',(3.65714815441855,1.53957527077174,-6.48522596314475));
#4589=CARTESIAN_POINT('Ctrl Pts',(3.59992408344123,1.54181718500802,-6.48227426546669));
#4590=CARTESIAN_POINT('Ctrl Pts',(3.54275550164339,1.54405692529934,-6.47932542999819));
#4591=CARTESIAN_POINT('Ctrl Pts',(3.48539653951463,1.54311529457029,-6.47637659452968));
#4592=CARTESIAN_POINT('Ctrl Pts',(3.42823038115855,1.53898142681884,-6.47342775906117));
#4593=CARTESIAN_POINT('Ctrl Pts',(3.37109712766582,1.5348499385233,-6.47048062094353));
#4594=CARTESIAN_POINT('Ctrl Pts',(3.3141569821572,1.52752989286647,-6.46753348282588));
#4595=CARTESIAN_POINT('Ctrl Pts',(3.25779148941335,1.51706248433199,-6.46458634470824));
#4596=CARTESIAN_POINT('Ctrl Pts',(3.20143622917433,1.50659697603476,-6.46163974160951));
#4597=CARTESIAN_POINT('Ctrl Pts',(3.14565593190065,1.49298533599691,-6.45869313851079));
#4598=CARTESIAN_POINT('Ctrl Pts',(3.09082310807727,1.47632007075786,-6.45574653541206));
#4599=CARTESIAN_POINT('Ctrl Pts',(3.03594089558616,1.4596397948885,-6.45279727826798));
#4600=CARTESIAN_POINT('Ctrl Pts',(2.98200836571185,1.43990055421428,-6.4498480211239));
#4601=CARTESIAN_POINT('Ctrl Pts',(2.92938251822518,1.41724465498291,-6.44689876397981));
#4602=CARTESIAN_POINT('Ctrl Pts',(2.87673184203508,1.39457806677208,-6.44394811538582));
#4603=CARTESIAN_POINT('Ctrl Pts',(2.82538954798554,1.36899231429978,-6.44099746679182));
#4604=CARTESIAN_POINT('Ctrl Pts',(2.77568933676639,1.34067638471604,-6.43804681819783));
#4605=CARTESIAN_POINT('Ctrl Pts',(2.7258998292641,1.31230957995083,-6.43509086817863));
#4606=CARTESIAN_POINT('Ctrl Pts',(2.67775873799462,1.28120309021216,-6.43213491815943));
#4607=CARTESIAN_POINT('Ctrl Pts',(2.63157094440542,1.24758937025734,-6.42917896814024));
#4608=CARTESIAN_POINT('Ctrl Pts',(2.60218002465184,1.22619977640494,-6.42729799303711));
#4609=CARTESIAN_POINT('Ctrl Pts',(2.57357939911721,1.20379579159119,-6.42541701793398));
#4610=CARTESIAN_POINT('Ctrl Pts',(2.54584005379241,1.18044527685753,-6.42353604283085));
#4611=CARTESIAN_POINT('Ctrl Pts',(2.5025987241781,1.1440454522604,-6.42060389488437));
#4612=CARTESIAN_POINT('Ctrl Pts',(2.46126130737398,1.10518307986427,-6.41767174693789));
#4613=CARTESIAN_POINT('Ctrl Pts',(2.42212621493193,1.06408752045743,-6.41473959899141));
#4614=CARTESIAN_POINT('Ctrl Pts',(2.38304397962318,1.02304746605458,-6.41181141129966));
#4615=CARTESIAN_POINT('Ctrl Pts',(2.346158547839,0.979780578008112,-6.4088832236079));
#4616=CARTESIAN_POINT('Ctrl Pts',(2.31173475047303,0.934555890675563,-6.40595503591615));
#4617=CARTESIAN_POINT('Ctrl Pts',(2.27734338470286,0.889373810751027,-6.40302960694967));
#4618=CARTESIAN_POINT('Ctrl Pts',(2.24540938426969,0.842238007844451,-6.40010417798319));
#4619=CARTESIAN_POINT('Ctrl Pts',(2.21615855693819,0.79345195461582,-6.39717874901671));
#4620=CARTESIAN_POINT('Ctrl Pts',(2.18692334329738,0.744691942713686,-6.39425488160411));
#4621=CARTESIAN_POINT('Ctrl Pts',(2.16036873932762,0.694283884801881,-6.39133101419151));
#4622=CARTESIAN_POINT('Ctrl Pts',(2.1366769243486,0.642559700970342,-6.38840714677891));
#4623=CARTESIAN_POINT('Ctrl Pts',(2.1129737029059,0.590810614444568,-6.38548187166549));
#4624=CARTESIAN_POINT('Ctrl Pts',(2.09213625856676,0.537744618682926,-6.38255659655207));
#4625=CARTESIAN_POINT('Ctrl Pts',(2.07429971023128,0.483716120393116,-6.37963132143865));
#4626=CARTESIAN_POINT('Ctrl Pts',(2.05645979752164,0.429677431113449,-6.37670549455255));
#4627=CARTESIAN_POINT('Ctrl Pts',(2.04162205759539,0.374676393092577,-6.37377966766645));
#4628=CARTESIAN_POINT('Ctrl Pts',(2.02987153650266,0.319082095571282,-6.37085384078036));
#4629=CARTESIAN_POINT('Ctrl Pts',(2.0181021161795,0.26339838163765,-6.36792330807091));
#4630=CARTESIAN_POINT('Ctrl Pts',(2.00942992235938,0.207120032030301,-6.36499277536147));
#4631=CARTESIAN_POINT('Ctrl Pts',(2.00388848089591,0.15062454625301,-6.36206224265202));
#4632=CARTESIAN_POINT('Ctrl Pts',(1.99894021196776,0.100176506930577,-6.35944540296426));
#4633=CARTESIAN_POINT('Ctrl Pts',(1.99648759434767,0.0495556759557013,-6.35682856327649));
#4634=CARTESIAN_POINT('Ctrl Pts',(1.99651935528198,-0.000969945748597822,
-6.35421172358872));
#4635=CARTESIAN_POINT('Ctrl Pts',(1.99491409331847,-0.000970954833059484,
-6.35421172358872));
#4636=CARTESIAN_POINT('Ctrl Pts',(1.99443510396552,-0.0638581426144525,
-6.35095805143182));
#4637=CARTESIAN_POINT('Ctrl Pts',(2.02640462481052,-0.635796929598567,-6.32134260070397));
#4638=CARTESIAN_POINT('Ctrl Pts',(2.7401727925123,-1.63684014941779,-6.26536537140521));
#4639=CARTESIAN_POINT('Ctrl Pts',(3.96445470277286,-1.58450089972216,-6.20956076318621));
#4640=CARTESIAN_POINT('Ctrl Pts',(4.4335630505712,-1.26162659872001,-6.18011793353816));
#4641=CARTESIAN_POINT('Ctrl Pts',(4.4805026613161,-1.22496740309806,-6.17703688246106));
#4642=CARTESIAN_POINT('Origin',(3.53951905042299,8.32667268468867E-16,-6.5));
#4643=CARTESIAN_POINT('',(3.98033068508385,1.1851773507571,-5.34783926643463));
#4644=CARTESIAN_POINT('',(3.98033068509731,1.1851773507521,-5.20988106086703));
#4645=CARTESIAN_POINT('',(3.98033068509731,1.1851773507521,-6.5));
#4646=CARTESIAN_POINT('',(2.27502014636762,0.00166482514493488,-5.05658113604771));
#4647=CARTESIAN_POINT('Ctrl Pts',(3.98033068509731,1.1851773507521,-5.20988106086703));
#4648=CARTESIAN_POINT('Ctrl Pts',(3.93383793648786,1.20246973699456,-5.20676616267198));
#4649=CARTESIAN_POINT('Ctrl Pts',(3.88629663681185,1.21703326229598,-5.20365126447694));
#4650=CARTESIAN_POINT('Ctrl Pts',(3.83805721807373,1.22875351981418,-5.20053636628189));
#4651=CARTESIAN_POINT('Ctrl Pts',(3.7898260992678,1.24047176077942,-5.19742200402705));
#4652=CARTESIAN_POINT('Ctrl Pts',(3.7408976307118,1.24934757713148,-5.19430764177221));
#4653=CARTESIAN_POINT('Ctrl Pts',(3.69163490741804,1.25531709780862,-5.19119327951737));
#4654=CARTESIAN_POINT('Ctrl Pts',(3.64232470727583,1.26129237159906,-5.18807591580229));
#4655=CARTESIAN_POINT('Ctrl Pts',(3.59268015271285,1.26435569180074,-5.18495855208722));
#4656=CARTESIAN_POINT('Ctrl Pts',(3.54307018622395,1.26449501360603,-5.18184118837215));
#4657=CARTESIAN_POINT('Ctrl Pts',(3.49343414586118,1.26463440863571,-5.17872218624137));
#4658=CARTESIAN_POINT('Ctrl Pts',(3.44383327594736,1.2618467746437,-5.17560318411059));
#4659=CARTESIAN_POINT('Ctrl Pts',(3.394633694541,1.25617215526016,-5.17248418197981));
#4660=CARTESIAN_POINT('Ctrl Pts',(3.34534262492254,1.25048698373843,-5.16935937996374));
#4661=CARTESIAN_POINT('Ctrl Pts',(3.29645487202891,1.24190420480259,-5.16623457794767));
#4662=CARTESIAN_POINT('Ctrl Pts',(3.24832704708739,1.2305151227,-5.1631097759316));
#4663=CARTESIAN_POINT('Ctrl Pts',(3.22296988250465,1.22451454341614,-5.16146340776295));
#4664=CARTESIAN_POINT('Ctrl Pts',(3.1978234261036,1.21773579564166,-5.1598170395943));
#4665=CARTESIAN_POINT('Ctrl Pts',(3.17293779691212,1.21019768408901,-5.15817067142565));
#4666=CARTESIAN_POINT('Ctrl Pts',(3.12623148321434,1.19604986406976,-5.15508070381603));
#4667=CARTESIAN_POINT('Ctrl Pts',(3.08023135044039,1.17915948645447,-5.1519907362064));
#4668=CARTESIAN_POINT('Ctrl Pts',(3.03528596549808,1.1596159907776,-5.14890076859677));
#4669=CARTESIAN_POINT('Ctrl Pts',(2.99042256294068,1.1401081433077,-5.14581643722575));
#4670=CARTESIAN_POINT('Ctrl Pts',(2.94661060463452,1.11795698926683,-5.14273210585473));
#4671=CARTESIAN_POINT('Ctrl Pts',(2.90418287418204,1.09330151063626,-5.1396477744837));
#4672=CARTESIAN_POINT('Ctrl Pts',(2.86179747117057,1.06867062920442,-5.1365665201534));
#4673=CARTESIAN_POINT('Ctrl Pts',(2.82079404657099,1.04154064457733,-5.1334852658231));
#4674=CARTESIAN_POINT('Ctrl Pts',(2.78148262924307,1.01209734421385,-5.13040401149279));
#4675=CARTESIAN_POINT('Ctrl Pts',(2.74219287983153,0.982670272595451,-5.1273244555078));
#4676=CARTESIAN_POINT('Ctrl Pts',(2.70459373924722,0.950932744232993,-5.1242448995228));
#4677=CARTESIAN_POINT('Ctrl Pts',(2.66896563574984,0.917113407491636,-5.12116534353781));
#4678=CARTESIAN_POINT('Ctrl Pts',(2.63334126514557,0.883297614131952,-5.11808611020971));
#4679=CARTESIAN_POINT('Ctrl Pts',(2.5996879267293,0.847400831915252,-5.11500687688161));
#4680=CARTESIAN_POINT('Ctrl Pts',(2.56825029767131,0.809689607150916,-5.11192764355352));
#4681=CARTESIAN_POINT('Ctrl Pts',(2.53677682467762,0.771935385546272,-5.10884489940591));
#4682=CARTESIAN_POINT('Ctrl Pts',(2.50752446118266,0.7323630247258,-5.1057621552583));
#4683=CARTESIAN_POINT('Ctrl Pts',(2.48069730103542,0.691271837285332,-5.10267941111069));
#4684=CARTESIAN_POINT('Ctrl Pts',(2.45385343030684,0.650155054231102,-5.09959474672827));
#4685=CARTESIAN_POINT('Ctrl Pts',(2.42943804360905,0.607518050553414,-5.09651008234585));
#4686=CARTESIAN_POINT('Ctrl Pts',(2.40760963429149,0.563685482936052,-5.09342541796343));
#4687=CARTESIAN_POINT('Ctrl Pts',(2.38573573195641,0.519761563001731,-5.09033432477125));
#4688=CARTESIAN_POINT('Ctrl Pts',(2.36645978141159,0.474637623744029,-5.08724323157908));
#4689=CARTESIAN_POINT('Ctrl Pts',(2.34989178961744,0.428657474387527,-5.0841521383869));
#4690=CARTESIAN_POINT('Ctrl Pts',(2.3408392484497,0.403534502326666,-5.08246320416221));
#4691=CARTESIAN_POINT('Ctrl Pts',(2.33259425763629,0.378156169768814,-5.08077426993752));
#4692=CARTESIAN_POINT('Ctrl Pts',(2.32516831107601,0.352579823369751,-5.07908533571283));
#4693=CARTESIAN_POINT('Ctrl Pts',(2.30700791862498,0.290032041171172,-5.07495499245014));
#4694=CARTESIAN_POINT('Ctrl Pts',(2.2936812592166,0.226070765504886,-5.07082464918745));
#4695=CARTESIAN_POINT('Ctrl Pts',(2.28535400033502,0.161339013068296,-5.06669430592475));
#4696=CARTESIAN_POINT('Ctrl Pts',(2.27855755281454,0.108506986995674,-5.06332324929907));
#4697=CARTESIAN_POINT('Ctrl Pts',(2.27509057994272,0.0551618418107654,-5.05995219267339));
#4698=CARTESIAN_POINT('Ctrl Pts',(2.27502014636762,0.00166482514493488,
-5.05658113604771));
#4699=CARTESIAN_POINT('',(2.58140289770062,-0.825211298936501,-5.));
#4700=CARTESIAN_POINT('Ctrl Pts',(2.27502018610934,0.00169474171970803,
-5.05612766244439));
#4701=CARTESIAN_POINT('Ctrl Pts',(2.27492762199581,-0.067370187214906,-5.05136691138681));
#4702=CARTESIAN_POINT('Ctrl Pts',(2.28049343395356,-0.136334638631543,-5.0466822093755));
#4703=CARTESIAN_POINT('Ctrl Pts',(2.2980708935941,-0.243587770328582,-5.0395587692782));
#4704=CARTESIAN_POINT('Ctrl Pts',(2.30630841992252,-0.282348371496498,-5.03701662818025));
#4705=CARTESIAN_POINT('Ctrl Pts',(2.32685863727146,-0.360737280072117,-5.03192125490839));
#4706=CARTESIAN_POINT('Ctrl Pts',(2.33932850452305,-0.400274698986001,-5.02937610304411));
#4707=CARTESIAN_POINT('Ctrl Pts',(2.37034907125676,-0.484040487389494,-5.02398385765428));
#4708=CARTESIAN_POINT('Ctrl Pts',(2.38951839495634,-0.527970216674481,-5.02115625735706));
#4709=CARTESIAN_POINT('Ctrl Pts',(2.44620717420155,-0.640053277041579,-5.01378604101922));
#4710=CARTESIAN_POINT('Ctrl Pts',(2.48759504636693,-0.706012164800675,-5.00929109021215));
#4711=CARTESIAN_POINT('Ctrl Pts',(2.54975148458737,-0.787355859854348,-5.00307314010455));
#4712=CARTESIAN_POINT('Ctrl Pts',(2.56530247076859,-0.806517809003463,-5.00155260994088));
#4713=CARTESIAN_POINT('Ctrl Pts',(2.58140289770062,-0.825211298936505,-5.));
#4714=CARTESIAN_POINT('',(4.48475997009368,-0.83992848134833,-5.));
#4715=CARTESIAN_POINT('Origin',(3.53951905042299,8.32667268468867E-16,-5.));
#4716=CARTESIAN_POINT('Ctrl Pts',(4.48475997009368,-0.83992848134833,-5.));
#4717=CARTESIAN_POINT('Ctrl Pts',(4.4743645141033,-0.851627346905269,-5.0010238610782));
#4718=CARTESIAN_POINT('Ctrl Pts',(4.46375282341081,-0.863132148146834,-5.00206025069617));
#4719=CARTESIAN_POINT('Ctrl Pts',(4.40421107071591,-0.925327730920914,-5.00781443230508));
#4720=CARTESIAN_POINT('Ctrl Pts',(4.35132615145554,-0.97205564021386,-5.01269719730609));
#4721=CARTESIAN_POINT('Ctrl Pts',(4.25291556543452,-1.04535004341478,-5.02111726956437));
#4722=CARTESIAN_POINT('Ctrl Pts',(4.20910528876381,-1.07393968753869,-5.02467043786506));
#4723=CARTESIAN_POINT('Ctrl Pts',(4.12654471049289,-1.12079487791517,-5.03097376948309));
#4724=CARTESIAN_POINT('Ctrl Pts',(4.0883967039719,-1.13996241146875,-5.03374816690764));
#4725=CARTESIAN_POINT('Ctrl Pts',(4.0174102350422,-1.17123795030084,-5.0386725547192));
#4726=CARTESIAN_POINT('Ctrl Pts',(3.98490083149402,-1.18398216322048,-5.0408424334626));
#4727=CARTESIAN_POINT('Ctrl Pts',(3.89903290236951,-1.21360535989443,-5.04638289410142));
#4728=CARTESIAN_POINT('Ctrl Pts',(3.84500778793352,-1.22831829455146,-5.04968091607328));
#4729=CARTESIAN_POINT('Ctrl Pts',(3.71808637329925,-1.2539873051317,-5.0571950936033));
#4730=CARTESIAN_POINT('Ctrl Pts',(3.64486043657265,-1.26224916290169,-5.06135580064609));
#4731=CARTESIAN_POINT('Ctrl Pts',(3.54245933434724,-1.26482643100954,-5.06734893032052));
#4732=CARTESIAN_POINT('Ctrl Pts',(3.5135696546245,-1.26456354629239,-5.06906017420318));
#4733=CARTESIAN_POINT('Ctrl Pts',(3.46109229551139,-1.26228706604992,-5.0722450323917));
#4734=CARTESIAN_POINT('Ctrl Pts',(3.43750362481475,-1.26059988191603,-5.07370488792634));
#4735=CARTESIAN_POINT('Ctrl Pts',(3.39105407348582,-1.25596542288288,-5.07665963921581));
#4736=CARTESIAN_POINT('Ctrl Pts',(3.36819912874026,-1.25305237762915,-5.07815265257495));
#4737=CARTESIAN_POINT('Ctrl Pts',(3.2965384961007,-1.24192175199295,-5.08293167075412));
#4738=CARTESIAN_POINT('Ctrl Pts',(3.24813003345425,-1.23146287712779,-5.08630237284614));
#4739=CARTESIAN_POINT('Ctrl Pts',(3.13401621803822,-1.19970202365469,-5.09442626540856));
#4740=CARTESIAN_POINT('Ctrl Pts',(3.06918849400282,-1.17580097531217,-5.09918282320499));
#4741=CARTESIAN_POINT('Ctrl Pts',(2.96247804631192,-1.12621242059119,-5.10708133864211));
#4742=CARTESIAN_POINT('Ctrl Pts',(2.9195427603486,-1.10315961359804,-5.11028233747527));
#4743=CARTESIAN_POINT('Ctrl Pts',(2.84880332620626,-1.05973997347714,-5.11559260274478));
#4744=CARTESIAN_POINT('Ctrl Pts',(2.82030757361024,-1.04061147451596,-5.11774329065059));
#4745=CARTESIAN_POINT('Ctrl Pts',(2.75620244933123,-0.993686332871481,-5.12262750419393));
#4746=CARTESIAN_POINT('Ctrl Pts',(2.72123327068826,-0.965094023148555,-5.125326492505));
#4747=CARTESIAN_POINT('Ctrl Pts',(2.60903907537223,-0.862866940372734,-5.13423063660923));
#4748=CARTESIAN_POINT('Ctrl Pts',(2.53962259610747,-0.781368418606664,-5.14013376231597));
#4749=CARTESIAN_POINT('Ctrl Pts',(2.4632036049359,-0.664525024115634,-5.14836345464608));
#4750=CARTESIAN_POINT('Ctrl Pts',(2.44623638784157,-0.636224064089069,-5.15034459662317));
#4751=CARTESIAN_POINT('Ctrl Pts',(2.42079093564898,-0.589752213326867,-5.15363129948203));
#4752=CARTESIAN_POINT('Ctrl Pts',(2.4116048890828,-0.57198758318919,-5.15489678252057));
#4753=CARTESIAN_POINT('Ctrl Pts',(2.38915256413399,-0.525921738428734,-5.15820497132823));
#4754=CARTESIAN_POINT('Ctrl Pts',(2.37650884762872,-0.497336543800919,-5.1602785064423));
#4755=CARTESIAN_POINT('Ctrl Pts',(2.33313051466738,-0.38853938817627,-5.16817180977536));
#4756=CARTESIAN_POINT('Ctrl Pts',(2.30953313212375,-0.305730994533581,-5.17416419262342));
#4757=CARTESIAN_POINT('Ctrl Pts',(2.28721462895428,-0.180094801583148,-5.18282841741911));
#4758=CARTESIAN_POINT('Ctrl Pts',(2.28195466443356,-0.138682650408762,-5.18562148923988));
#4759=CARTESIAN_POINT('Ctrl Pts',(2.27587380190061,-0.0597133732315236,
-5.19081296811046));
#4760=CARTESIAN_POINT('Ctrl Pts',(2.27465888365585,-0.0222316917080967,
-5.1932202476294));
#4761=CARTESIAN_POINT('Ctrl Pts',(2.27553710499034,0.0505733384564403,-5.1977955046571));
#4762=CARTESIAN_POINT('Ctrl Pts',(2.27744304036795,0.0858635505184319,-5.19996731003112));
#4763=CARTESIAN_POINT('Ctrl Pts',(2.28804875130298,0.19616088358106,-5.20664995369242));
#4764=CARTESIAN_POINT('Ctrl Pts',(2.30198506044707,0.270496428041747,-5.21099058531991));
#4765=CARTESIAN_POINT('Ctrl Pts',(2.33773738553142,0.397298403786643,-5.21852052734508));
#4766=CARTESIAN_POINT('Ctrl Pts',(2.35659993548028,0.450363089996163,-5.22171668726163));
#4767=CARTESIAN_POINT('Ctrl Pts',(2.39279803420042,0.534051715336838,-5.22706607770719));
#4768=CARTESIAN_POINT('Ctrl Pts',(2.4079858052802,0.565519558930165,-5.22915375780192));
#4769=CARTESIAN_POINT('Ctrl Pts',(2.43388776422174,0.613954250597111,-5.23255070019152));
#4770=CARTESIAN_POINT('Ctrl Pts',(2.4437359266768,0.631363294207987,-5.23381224779747));
#4771=CARTESIAN_POINT('Ctrl Pts',(2.46919692470231,0.673980350977448,-5.23700803109764));
#4772=CARTESIAN_POINT('Ctrl Pts',(2.48528903118701,0.698883192109106,-5.23896782302949));
#4773=CARTESIAN_POINT('Ctrl Pts',(2.55114631917314,0.793342341460392,-5.24670165190081));
#4774=CARTESIAN_POINT('Ctrl Pts',(2.60704166538098,0.858346627924565,-5.25266507426581));
#4775=CARTESIAN_POINT('Ctrl Pts',(2.70040320575373,0.94694815151863,-5.26141964091538));
#4776=CARTESIAN_POINT('Ctrl Pts',(2.73324154547406,0.975060710863728,-5.26431831772141));
#4777=CARTESIAN_POINT('Ctrl Pts',(2.79780873090725,1.02483891266637,-5.269672645021));
#4778=CARTESIAN_POINT('Ctrl Pts',(2.82921055875536,1.04684829775139,-5.27213882732288));
#4779=CARTESIAN_POINT('Ctrl Pts',(2.8914676395768,1.0863905158672,-5.27678094391539));
#4780=CARTESIAN_POINT('Ctrl Pts',(2.9221552813526,1.10411835666648,-5.27896272802317));
#4781=CARTESIAN_POINT('Ctrl Pts',(3.01270516141864,1.15147024643782,-5.28513697804023));
#4782=CARTESIAN_POINT('Ctrl Pts',(3.07422041368736,1.17767362145201,-5.28900896875804));
#4783=CARTESIAN_POINT('Ctrl Pts',(3.21462029992273,1.22475031791382,-5.29750616966733));
#4784=CARTESIAN_POINT('Ctrl Pts',(3.29402373486489,1.24310177739744,-5.30209051974957));
#4785=CARTESIAN_POINT('Ctrl Pts',(3.40040308794286,1.25709297651745,-5.30852607071481));
#4786=CARTESIAN_POINT('Ctrl Pts',(3.42627259895793,1.25968687097981,-5.310114481789));
#4787=CARTESIAN_POINT('Ctrl Pts',(3.47308082785827,1.26292685993581,-5.31306001010594));
#4788=CARTESIAN_POINT('Ctrl Pts',(3.49398942685692,1.2638532744479,-5.314403271179));
#4789=CARTESIAN_POINT('Ctrl Pts',(3.55495672925024,1.26504005998883,-5.31838627957415));
#4790=CARTESIAN_POINT('Ctrl Pts',(3.5950153476632,1.26391623423788,-5.32108418100623));
#4791=CARTESIAN_POINT('Ctrl Pts',(3.71404739847578,1.25490736348001,-5.32922380939964));
#4792=CARTESIAN_POINT('Ctrl Pts',(3.79241350516521,1.2414903899723,-5.33473260426232));
#4793=CARTESIAN_POINT('Ctrl Pts',(3.90629091016403,1.2107559904635,-5.34268783329034));
#4794=CARTESIAN_POINT('Ctrl Pts',(3.94309777202561,1.19898972085493,-5.34525373164033));
#4795=CARTESIAN_POINT('Ctrl Pts',(3.97965115673757,1.18542992638994,-5.34779208082771));
#4796=CARTESIAN_POINT('Ctrl Pts',(3.97999094872115,1.18530371137418,-5.34781567595674));
#4797=CARTESIAN_POINT('Ctrl Pts',(3.98033068508385,1.1851773507571,-5.34783926643463));
#4798=CARTESIAN_POINT('Origin',(3.53951905042299,8.32667268468867E-16,-6.5));
#4799=CARTESIAN_POINT('',(3.98033068509731,1.1851773507521,-5.8467115517674));
#4800=CARTESIAN_POINT('',(3.98033068509731,1.1851773507521,-5.70990589948393));
#4801=CARTESIAN_POINT('',(3.98033068509731,1.1851773507521,-6.5));
#4802=CARTESIAN_POINT('',(2.27501908476962,-0.00029472464996097,-5.55658032642993));
#4803=CARTESIAN_POINT('Ctrl Pts',(3.98033068509731,1.1851773507521,-5.70990589948393));
#4804=CARTESIAN_POINT('Ctrl Pts',(3.93266078708269,1.20290756273704,-5.70668826557637));
#4805=CARTESIAN_POINT('Ctrl Pts',(3.88381723853165,1.21779517476562,-5.70347063166882));
#4806=CARTESIAN_POINT('Ctrl Pts',(3.83417275920534,1.22969079117508,-5.70025299776126));
#4807=CARTESIAN_POINT('Ctrl Pts',(3.7861066381084,1.24120820754482,-5.6971376628208));
#4808=CARTESIAN_POINT('Ctrl Pts',(3.7372903345029,1.24992090283827,-5.69402232788034));
#4809=CARTESIAN_POINT('Ctrl Pts',(3.68808057068957,1.25574269844427,-5.69090699293988));
#4810=CARTESIAN_POINT('Ctrl Pts',(3.63891548683514,1.2615592081564,-5.68779448656486));
#4811=CARTESIAN_POINT('Ctrl Pts',(3.58935819208574,1.26448995114612,-5.68468198018984));
#4812=CARTESIAN_POINT('Ctrl Pts',(3.53977466164734,1.26449997416485,-5.68156947381481));
#4813=CARTESIAN_POINT('Ctrl Pts',(3.49021507007097,1.26450999234448,-5.6784584701537));
#4814=CARTESIAN_POINT('Ctrl Pts',(3.44062981503274,1.26160208493541,-5.67534746649258));
#4815=CARTESIAN_POINT('Ctrl Pts',(3.3913864360269,1.25579336618418,-5.67223646283146));
#4816=CARTESIAN_POINT('Ctrl Pts',(3.34214589715217,1.24998498245306,-5.66912563859869));
#4817=CARTESIAN_POINT('Ctrl Pts',(3.2932477386714,1.2412761865991,-5.66601481436593));
#4818=CARTESIAN_POINT('Ctrl Pts',(3.2450533364277,1.22973582255753,-5.66290399013316));
#4819=CARTESIAN_POINT('Ctrl Pts',(3.19680873819873,1.21818343886396,-5.65978992587914));
#4820=CARTESIAN_POINT('Ctrl Pts',(3.14926989168937,1.20379373299775,-5.65667586162512));
#4821=CARTESIAN_POINT('Ctrl Pts',(3.10278512137278,1.18668602638455,-5.65356179737111));
#4822=CARTESIAN_POINT('Ctrl Pts',(3.05627090213853,1.16956748173904,-5.65044576030274));
#4823=CARTESIAN_POINT('Ctrl Pts',(3.01081258962835,1.149727730013,-5.64732972323438));
#4824=CARTESIAN_POINT('Ctrl Pts',(2.96673728188377,1.12733371085455,-5.64421368616602));
#4825=CARTESIAN_POINT('Ctrl Pts',(2.9225839425669,1.10490004499561,-5.64109213241985));
#4826=CARTESIAN_POINT('Ctrl Pts',(2.87981896217944,1.07990337102618,-5.63797057867369));
#4827=CARTESIAN_POINT('Ctrl Pts',(2.83874208093206,1.0525549339731,-5.63484902492752));
#4828=CARTESIAN_POINT('Ctrl Pts',(2.82923971273982,1.04622838457428,-5.63412691185255));
#4829=CARTESIAN_POINT('Ctrl Pts',(2.81982754314012,1.0397761536681,-5.63340479877757));
#4830=CARTESIAN_POINT('Ctrl Pts',(2.81050902345375,1.03320115688007,-5.6326826857026));
#4831=CARTESIAN_POINT('Ctrl Pts',(2.76958968560826,1.00432913385951,-5.62951175406624));
#4832=CARTESIAN_POINT('Ctrl Pts',(2.73029110202993,0.972953837852343,-5.62634082242988));
#4833=CARTESIAN_POINT('Ctrl Pts',(2.69293720100625,0.939286656052421,-5.62316989079352));
#4834=CARTESIAN_POINT('Ctrl Pts',(2.65645656039763,0.906406546455044,-5.62007308927479));
#4835=CARTESIAN_POINT('Ctrl Pts',(2.62183110828954,0.871340933996097,-5.61697628775606));
#4836=CARTESIAN_POINT('Ctrl Pts',(2.58933297529691,0.83433007415321,-5.61387948623733));
#4837=CARTESIAN_POINT('Ctrl Pts',(2.5568668743894,0.797355694406365,-5.61078573710963));
#4838=CARTESIAN_POINT('Ctrl Pts',(2.52652430809794,0.758440276970468,-5.60769198798194));
#4839=CARTESIAN_POINT('Ctrl Pts',(2.49854077772478,0.717861049068864,-5.60459823885425));
#4840=CARTESIAN_POINT('Ctrl Pts',(2.47057254586883,0.677304005716816,-5.60150618107048));
#4841=CARTESIAN_POINT('Ctrl Pts',(2.44496111038932,0.635085410031833,-5.59841412328672));
#4842=CARTESIAN_POINT('Ctrl Pts',(2.42190017579619,0.591513567957594,-5.59532206550296));
#4843=CARTESIAN_POINT('Ctrl Pts',(2.39782180110025,0.546019351952645,-5.59209358724687));
#4844=CARTESIAN_POINT('Ctrl Pts',(2.37652462727331,0.499050215905228,-5.58886510899079));
#4845=CARTESIAN_POINT('Ctrl Pts',(2.35817563284779,0.450985564903965,-5.5856366307347));
#4846=CARTESIAN_POINT('Ctrl Pts',(2.34058627219792,0.40491075222674,-5.5825418089107));
#4847=CARTESIAN_POINT('Ctrl Pts',(2.32570585877347,0.357829942193402,-5.5794469870867));
#4848=CARTESIAN_POINT('Ctrl Pts',(2.31363092908186,0.310094443605026,-5.5763521652627));
#4849=CARTESIAN_POINT('Ctrl Pts',(2.30154836761841,0.262328774535878,-5.57325538740461));
#4850=CARTESIAN_POINT('Ctrl Pts',(2.29227491914344,0.213908139602331,-5.57015860954653));
#4851=CARTESIAN_POINT('Ctrl Pts',(2.28585581517434,0.165193046421117,-5.56706183168844));
#4852=CARTESIAN_POINT('Ctrl Pts',(2.27942574158406,0.116394703907808,-5.56395976173973));
#4853=CARTESIAN_POINT('Ctrl Pts',(2.27585977127268,0.0673014528084192,-5.56085769179101));
#4854=CARTESIAN_POINT('Ctrl Pts',(2.27515112835769,0.0182758762383297,-5.55775562184229));
#4855=CARTESIAN_POINT('Ctrl Pts',(2.27506163276488,0.012084361520348,-5.55736385670483));
#4856=CARTESIAN_POINT('Ctrl Pts',(2.2750176423448,0.00589392001067389,-5.55697209156738));
#4857=CARTESIAN_POINT('Ctrl Pts',(2.27501908476962,-0.000294724649960815,
-5.55658032642993));
#4858=CARTESIAN_POINT('Ctrl Pts',(2.2750190847698,-0.000294725429491894,
-5.55658032638058));
#4859=CARTESIAN_POINT('Ctrl Pts',(2.27502274574772,-0.016001909103677,-5.55558600091698));
#4860=CARTESIAN_POINT('Ctrl Pts',(2.27531905952943,-0.0317053739536449,
-5.55459167545337));
#4861=CARTESIAN_POINT('Ctrl Pts',(2.27590767758865,-0.0473977683410977,
-5.55359734998976));
#4862=CARTESIAN_POINT('Ctrl Pts',(2.27775605165365,-0.096674908838074,-5.55047497654182));
#4863=CARTESIAN_POINT('Ctrl Pts',(2.28249527066355,-0.145951370989865,-5.54735260309388));
#4864=CARTESIAN_POINT('Ctrl Pts',(2.29012341262698,-0.194860951081293,-5.54423022964595));
#4865=CARTESIAN_POINT('Ctrl Pts',(2.2977376142519,-0.2436811494981,-5.54111356229827));
#4866=CARTESIAN_POINT('Ctrl Pts',(2.30823018369446,-0.292135258826107,-5.5379968949506));
#4867=CARTESIAN_POINT('Ctrl Pts',(2.32154730484888,-0.339860378660354,-5.53488022760293));
#4868=CARTESIAN_POINT('Ctrl Pts',(2.33485101052464,-0.387537420886852,-5.53176669994168));
#4869=CARTESIAN_POINT('Ctrl Pts',(2.35097348810582,-0.434486402446487,-5.52865317228042));
#4870=CARTESIAN_POINT('Ctrl Pts',(2.36980995915212,-0.480354964373507,-5.52553964461917));
#4871=CARTESIAN_POINT('Ctrl Pts',(2.38863545658795,-0.526196804536665,-5.52242793081359));
#4872=CARTESIAN_POINT('Ctrl Pts',(2.41017160734413,-0.570958966357735,-5.51931621700801));
#4873=CARTESIAN_POINT('Ctrl Pts',(2.43426475233936,-0.614307078396184,-5.51620450320243));
#4874=CARTESIAN_POINT('Ctrl Pts',(2.45835409572011,-0.657648350613166,-5.51309328038863));
#4875=CARTESIAN_POINT('Ctrl Pts',(2.48499936537833,-0.699575538115731,-5.50998205757484));
#4876=CARTESIAN_POINT('Ctrl Pts',(2.51400121246915,-0.73977930089891,-5.50687083476104));
#4877=CARTESIAN_POINT('Ctrl Pts',(2.54303116976748,-0.780022031410974,-5.5037565963766));
#4878=CARTESIAN_POINT('Ctrl Pts',(2.57442194269341,-0.818537557918219,-5.50064235799216));
#4879=CARTESIAN_POINT('Ctrl Pts',(2.60793219618554,-0.855047474127594,-5.49752811960771));
#4880=CARTESIAN_POINT('Ctrl Pts',(2.64146065504772,-0.891577225356572,-5.49441218932732));
#4881=CARTESIAN_POINT('Ctrl Pts',(2.67711049359016,-0.926098815186914,-5.49129625904692));
#4882=CARTESIAN_POINT('Ctrl Pts',(2.71460409784854,-0.958371311663225,-5.48818032876653));
#4883=CARTESIAN_POINT('Ctrl Pts',(2.75216641403445,-0.990702951705028,-5.48505868813686));
#4884=CARTESIAN_POINT('Ctrl Pts',(2.79157880363042,-1.02077694043359,-5.4819370475072));
#4885=CARTESIAN_POINT('Ctrl Pts',(2.83253258454186,-1.04839419449981,-5.47881540687754));
#4886=CARTESIAN_POINT('Ctrl Pts',(2.8513517695631,-1.0610849449625,-5.47738094267736));
#4887=CARTESIAN_POINT('Ctrl Pts',(2.87049606900254,-1.0732575561212,-5.47594647847717));
#4888=CARTESIAN_POINT('Ctrl Pts',(2.88993386662373,-1.08489600376648,-5.47451201427699));
#4889=CARTESIAN_POINT('Ctrl Pts',(2.93224490233421,-1.11022988075866,-5.4713895583701));
#4890=CARTESIAN_POINT('Ctrl Pts',(2.97613231701829,-1.13314001524391,-5.4682671024632));
#4891=CARTESIAN_POINT('Ctrl Pts',(3.02128805141708,-1.15342831665836,-5.46514464655631));
#4892=CARTESIAN_POINT('Ctrl Pts',(3.06636157543434,-1.17367968125798,-5.46202787538236));
#4893=CARTESIAN_POINT('Ctrl Pts',(3.11269834367567,-1.19131845758046,-5.45891110420842));
#4894=CARTESIAN_POINT('Ctrl Pts',(3.15996476984413,-1.20619185791244,-5.45579433303447));
#4895=CARTESIAN_POINT('Ctrl Pts',(3.20718378070552,-1.2210503379955,-5.45268068844898));
#4896=CARTESIAN_POINT('Ctrl Pts',(3.25533008322022,-1.23314877058989,-5.44956704386349));
#4897=CARTESIAN_POINT('Ctrl Pts',(3.30405114133481,-1.24238283704728,-5.44645339927799));
#4898=CARTESIAN_POINT('Ctrl Pts',(3.35274401589305,-1.25161156189587,-5.44334155583518));
#4899=CARTESIAN_POINT('Ctrl Pts',(3.40201045025828,-1.25797910157165,-5.44022971239238));
#4900=CARTESIAN_POINT('Ctrl Pts',(3.45148633478003,-1.26143192086475,-5.43711786894957));
#4901=CARTESIAN_POINT('Ctrl Pts',(3.50095460919738,-1.26488420906445,-5.43400650415315));
#4902=CARTESIAN_POINT('Ctrl Pts',(3.5506317237145,-1.26542263006767,-5.43089513935673));
#4903=CARTESIAN_POINT('Ctrl Pts',(3.60014963877545,-1.26304559765514,-5.42778377456031));
#4904=CARTESIAN_POINT('Ctrl Pts',(3.64971582044746,-1.26066624827715,-5.42466937702242));
#4905=CARTESIAN_POINT('Ctrl Pts',(3.69912194490598,-1.25536579956374,-5.42155497948453));
#4906=CARTESIAN_POINT('Ctrl Pts',(3.7480030070167,-1.24719472811708,-5.41844058194665));
#4907=CARTESIAN_POINT('Ctrl Pts',(3.79691078113621,-1.23901919142922,-5.41532448248554));
#4908=CARTESIAN_POINT('Ctrl Pts',(3.84529238718609,-1.22797003034951,-5.41220838302444));
#4909=CARTESIAN_POINT('Ctrl Pts',(3.89279445080751,-1.21414856647906,-5.40909228356333));
#4910=CARTESIAN_POINT('Ctrl Pts',(3.94038376461397,-1.2003017158109,-5.40597046055605));
#4911=CARTESIAN_POINT('Ctrl Pts',(3.98708979596454,-1.18367258409638,-5.40284863754878));
#4912=CARTESIAN_POINT('Ctrl Pts',(4.03257730729884,-1.16441135571865,-5.3997268145415));
#4913=CARTESIAN_POINT('Ctrl Pts',(4.05346280524401,-1.1555676020398,-5.39829343588236));
#4914=CARTESIAN_POINT('Ctrl Pts',(4.07409174376038,-1.14616960703868,-5.39686005722323));
#4915=CARTESIAN_POINT('Ctrl Pts',(4.0944335217213,-1.13623508991041,-5.3954266785641));
#4916=CARTESIAN_POINT('Ctrl Pts',(4.13867888344531,-1.1146265410049,-5.3923089394273));
#4917=CARTESIAN_POINT('Ctrl Pts',(4.18175845816928,-1.09038172784545,-5.3891912002905));
#4918=CARTESIAN_POINT('Ctrl Pts',(4.22333876640782,-1.06364977602142,-5.3860734611537));
#4919=CARTESIAN_POINT('Ctrl Pts',(4.26484300037015,-1.03696673229772,-5.38296142615327));
#4920=CARTESIAN_POINT('Ctrl Pts',(4.30485294930259,-1.00780586895283,-5.37984939115284));
#4921=CARTESIAN_POINT('Ctrl Pts',(4.34305908348303,-0.976362466131235,-5.37673735615241));
#4922=CARTESIAN_POINT('Ctrl Pts',(4.3812267346318,-0.944950734597319,-5.37362845574133));
#4923=CARTESIAN_POINT('Ctrl Pts',(4.41759374531062,-0.911261362163879,-5.37051955533026));
#4924=CARTESIAN_POINT('Ctrl Pts',(4.4518808051329,-0.875531997440788,-5.36741065491918));
#4925=CARTESIAN_POINT('Ctrl Pts',(4.48614801060192,-0.839823322255751,-5.364303554756));
#4926=CARTESIAN_POINT('Ctrl Pts',(4.51833727133104,-0.802077390582719,-5.36119645459281));
#4927=CARTESIAN_POINT('Ctrl Pts',(4.54820548565155,-0.762569292186549,-5.35808935442962));
#4928=CARTESIAN_POINT('Ctrl Pts',(4.57806919277791,-0.723067155669058,-5.35498272313624));
#4929=CARTESIAN_POINT('Ctrl Pts',(4.60561221858689,-0.681803819158794,-5.35187609184285));
#4930=CARTESIAN_POINT('Ctrl Pts',(4.63063283820331,-0.639086028728283,-5.34876946054947));
#4931=CARTESIAN_POINT('Ctrl Pts',(4.6556783001173,-0.596325824957177,-5.34565974476576));
#4932=CARTESIAN_POINT('Ctrl Pts',(4.67819607889475,-0.552108760000173,-5.34255002898205));
#4933=CARTESIAN_POINT('Ctrl Pts',(4.69802973222386,-0.506767451750091,-5.33944031319835));
#4934=CARTESIAN_POINT('Ctrl Pts',(4.71787438600363,-0.461400995595288,-5.33632887265549));
#4935=CARTESIAN_POINT('Ctrl Pts',(4.73503176028608,-0.414909570772984,-5.33321743211263));
#4936=CARTESIAN_POINT('Ctrl Pts',(4.74939437995943,-0.367643763688562,-5.33010599156978));
#4937=CARTESIAN_POINT('Ctrl Pts',(4.76378382985173,-0.320289661294376,-5.32698873867284));
#4938=CARTESIAN_POINT('Ctrl Pts',(4.7753679784059,-0.272158824256545,-5.32387148577591));
#4939=CARTESIAN_POINT('Ctrl Pts',(4.78409020431963,-0.223613266351477,-5.32075423287897));
#4940=CARTESIAN_POINT('Ctrl Pts',(4.78820603162296,-0.200705681217004,-5.31928326953642));
#4941=CARTESIAN_POINT('Ctrl Pts',(4.79168534827568,-0.177705835991882,-5.31781230619386));
#4942=CARTESIAN_POINT('Ctrl Pts',(4.79452622970454,-0.154651963944089,-5.31634134285131));
#4943=CARTESIAN_POINT('Ctrl Pts',(4.80056628812567,-0.105636636311179,-5.31321389640666));
#4944=CARTESIAN_POINT('Ctrl Pts',(4.80374356326664,-0.0561614284076493,
-5.31008644996201));
#4945=CARTESIAN_POINT('Ctrl Pts',(4.80400188255505,-0.00658917622266315,
-5.30695900351735));
#4946=CARTESIAN_POINT('Ctrl Pts',(4.80425972737876,0.0428920247533582,-5.30383730137051));
#4947=CARTESIAN_POINT('Ctrl Pts',(4.80160924873279,0.092469374936108,-5.30071559922367));
#4948=CARTESIAN_POINT('Ctrl Pts',(4.79604603805036,0.141775101354518,-5.29759389707683));
#4949=CARTESIAN_POINT('Ctrl Pts',(4.79048847306251,0.191030791006713,-5.29447536291659));
#4950=CARTESIAN_POINT('Ctrl Pts',(4.78202408983974,0.240014862905859,-5.29135682875634));
#4951=CARTESIAN_POINT('Ctrl Pts',(4.77070046785673,0.288361868779224,-5.2882382945961));
#4952=CARTESIAN_POINT('Ctrl Pts',(4.75938356895954,0.336680169961623,-5.28512161197884));
#4953=CARTESIAN_POINT('Ctrl Pts',(4.7452109192292,0.384361624174091,-5.28200492936157));
#4954=CARTESIAN_POINT('Ctrl Pts',(4.72828121689885,0.431050764476334,-5.27888824674431));
#4955=CARTESIAN_POINT('Ctrl Pts',(4.71135443753347,0.477731843755436,-5.27577210223185));
#4956=CARTESIAN_POINT('Ctrl Pts',(4.69167173757609,0.523420436840053,-5.27265595771939));
#4957=CARTESIAN_POINT('Ctrl Pts',(4.66938091360084,0.567778495662066,-5.26953981320693));
#4958=CARTESIAN_POINT('Ctrl Pts',(4.64706929923758,0.612177926721152,-5.26642076230332));
#4959=CARTESIAN_POINT('Ctrl Pts',(4.62214495041812,0.655243857716199,-5.26330171139971));
#4960=CARTESIAN_POINT('Ctrl Pts',(4.59480205087727,0.696662069408267,-5.2601826604961));
#4961=CARTESIAN_POINT('Ctrl Pts',(4.56744481033775,0.738102004418964,-5.25706197369046));
#4962=CARTESIAN_POINT('Ctrl Pts',(4.53766681944526,0.77789206113148,-5.25394128688483));
#4963=CARTESIAN_POINT('Ctrl Pts',(4.50570408803224,0.815749179037295,-5.25082060007919));
#4964=CARTESIAN_POINT('Ctrl Pts',(4.47368430213115,0.853673873097775,-5.24769434274875));
#4965=CARTESIAN_POINT('Ctrl Pts',(4.4394723684359,0.889658346260538,-5.2445680854183));
#4966=CARTESIAN_POINT('Ctrl Pts',(4.40334168380365,0.923455850628115,-5.24144182808786));
#4967=CARTESIAN_POINT('Ctrl Pts',(4.38721627028579,0.938539947133523,-5.24004655443806));
#4968=CARTESIAN_POINT('Ctrl Pts',(4.37070910220634,0.95318895592024,-5.23865128078826));
#4969=CARTESIAN_POINT('Ctrl Pts',(4.35384646135687,0.967383645614151,-5.23725600713846));
#4970=CARTESIAN_POINT('Ctrl Pts',(4.31608428534962,0.999171215270337,-5.23413143314009));
#4971=CARTESIAN_POINT('Ctrl Pts',(4.27637765767766,1.02881208577837,-5.23100685914173));
#4972=CARTESIAN_POINT('Ctrl Pts',(4.23499993142354,1.05606183254708,-5.22788228514336));
#4973=CARTESIAN_POINT('Ctrl Pts',(4.19368748929417,1.08326858575311,-5.22476264097312));
#4974=CARTESIAN_POINT('Ctrl Pts',(4.15070962524876,1.10809139224436,-5.22164299680288));
#4975=CARTESIAN_POINT('Ctrl Pts',(4.10637220230447,1.13032639277424,-5.21852335263265));
#4976=CARTESIAN_POINT('Ctrl Pts',(4.06542982508554,1.15085879449505,-5.21564258871077));
#4977=CARTESIAN_POINT('Ctrl Pts',(4.02332876222096,1.16918476310038,-5.2127618247889));
#4978=CARTESIAN_POINT('Ctrl Pts',(3.98033068509731,1.1851773507521,-5.20988106086703));
#4979=CARTESIAN_POINT('',(2.27501952462653,0.00109510754574143,-5.69341967361942));
#4980=CARTESIAN_POINT('Ctrl Pts',(3.98033068508385,1.1851773507571,-5.34783926643463));
#4981=CARTESIAN_POINT('Ctrl Pts',(4.01383899306308,1.17271436198533,-5.35016600294365));
#4982=CARTESIAN_POINT('Ctrl Pts',(4.0468062752844,1.15883497555727,-5.35244677809117));
#4983=CARTESIAN_POINT('Ctrl Pts',(4.11262314463296,1.12777762618674,-5.35699420702988));
#4984=CARTESIAN_POINT('Ctrl Pts',(4.14539459441361,1.11051606334499,-5.35925521350175));
#4985=CARTESIAN_POINT('Ctrl Pts',(4.21235649313321,1.07139739845899,-5.36390131317071));
#4986=CARTESIAN_POINT('Ctrl Pts',(4.24634763115312,1.04928373059564,-5.36627499860472));
#4987=CARTESIAN_POINT('Ctrl Pts',(4.35505663752254,0.97087676199841,-5.37402900391421));
#4988=CARTESIAN_POINT('Ctrl Pts',(4.42458507856987,0.907941949608262,-5.37924200727832));
#4989=CARTESIAN_POINT('Ctrl Pts',(4.50588853312012,0.816053420441164,-5.38652725672441));
#4990=CARTESIAN_POINT('Ctrl Pts',(4.52447588503683,0.793519309361531,-5.38829391937243));
#4991=CARTESIAN_POINT('Ctrl Pts',(4.55452196213696,0.754409780389055,-5.39136623261555));
#4992=CARTESIAN_POINT('Ctrl Pts',(4.56639404836727,0.738168401294929,-5.39264571877438));
#4993=CARTESIAN_POINT('Ctrl Pts',(4.5985072796071,0.691961975534618,-5.39629287469257));
#4994=CARTESIAN_POINT('Ctrl Pts',(4.61785633603671,0.661404295057555,-5.39870838581128));
#4995=CARTESIAN_POINT('Ctrl Pts',(4.6658382957047,0.577912698047838,-5.40523711375543));
#4996=CARTESIAN_POINT('Ctrl Pts',(4.692049014446,0.523691383273651,-5.40940152559124));
#4997=CARTESIAN_POINT('Ctrl Pts',(4.74009679133558,0.403032350044958,-5.41829767247082));
#4998=CARTESIAN_POINT('Ctrl Pts',(4.76049353314704,0.336222944703702,-5.42299589415376));
#4999=CARTESIAN_POINT('Ctrl Pts',(4.78278760168466,0.233448391232862,-5.4298190597256));
#5000=CARTESIAN_POINT('Ctrl Pts',(4.78883921860845,0.198530528253468,-5.43207143502346));
#5001=CARTESIAN_POINT('Ctrl Pts',(4.79832045384951,0.125774158497969,-5.43664203584638));
#5002=CARTESIAN_POINT('Ctrl Pts',(4.80152802478373,0.0879426534074953,-5.43895106809916));
#5003=CARTESIAN_POINT('Ctrl Pts',(4.80471082561513,0.00754626257473869,
-5.44375345981939));
#5004=CARTESIAN_POINT('Ctrl Pts',(4.8042496130601,-0.03498833550617,-5.44623230076327));
#5005=CARTESIAN_POINT('Ctrl Pts',(4.79639705344158,-0.163001369958141,-5.45362764700549));
#5006=CARTESIAN_POINT('Ctrl Pts',(4.78245737643129,-0.247818402955921,-5.45842909637968));
#5007=CARTESIAN_POINT('Ctrl Pts',(4.75210217012925,-0.359897005900358,-5.46530399947366));
#5008=CARTESIAN_POINT('Ctrl Pts',(4.74310411347431,-0.388929738538274,-5.46713695065838));
#5009=CARTESIAN_POINT('Ctrl Pts',(4.72644682058844,-0.436537430765181,-5.47027283083785));
#5010=CARTESIAN_POINT('Ctrl Pts',(4.71937551365201,-0.455303229163825,-5.47154534477018));
#5011=CARTESIAN_POINT('Ctrl Pts',(4.6989965656696,-0.505717745451123,-5.47506323219359));
#5012=CARTESIAN_POINT('Ctrl Pts',(4.68484280513477,-0.537002417496111,-5.47735002698292));
#5013=CARTESIAN_POINT('Ctrl Pts',(4.6450535440025,-0.616200873231293,-5.48334451660414));
#5014=CARTESIAN_POINT('Ctrl Pts',(4.61757073058802,-0.663109578273905,-5.48709603000919));
#5015=CARTESIAN_POINT('Ctrl Pts',(4.54326497476591,-0.773044751477453,-5.49620791905494));
#5016=CARTESIAN_POINT('Ctrl Pts',(4.49342271089991,-0.833771799768242,-5.50151597657881));
#5017=CARTESIAN_POINT('Ctrl Pts',(4.41331640010028,-0.914711308259354,-5.50890506251307));
#5018=CARTESIAN_POINT('Ctrl Pts',(4.38731162387462,-0.938864607305538,-5.51116097468996));
#5019=CARTESIAN_POINT('Ctrl Pts',(4.33142469063804,-0.986554067352629,-5.51573797273894));
#5020=CARTESIAN_POINT('Ctrl Pts',(4.30142770909568,-1.00990054807934,-5.51804987940183));
#5021=CARTESIAN_POINT('Ctrl Pts',(4.23568619295422,-1.05646748778856,-5.5228589219122));
#5022=CARTESIAN_POINT('Ctrl Pts',(4.19972804002095,-1.07930382153396,-5.52534149384131));
#5023=CARTESIAN_POINT('Ctrl Pts',(4.07025073296527,-1.15263558984765,-5.53392298603898));
#5024=CARTESIAN_POINT('Ctrl Pts',(3.97160330547309,-1.19312259814339,-5.53981654639278));
#5025=CARTESIAN_POINT('Ctrl Pts',(3.84840599039205,-1.22637981534584,-5.54761004845566));
#5026=CARTESIAN_POINT('Ctrl Pts',(3.82759943302925,-1.23143340518724,-5.54894173074041));
#5027=CARTESIAN_POINT('Ctrl Pts',(3.78257944721993,-1.24116462084355,-5.55187437396506));
#5028=CARTESIAN_POINT('Ctrl Pts',(3.75833873242266,-1.24566677385104,-5.55348273678575));
#5029=CARTESIAN_POINT('Ctrl Pts',(3.70336636963696,-1.25422265243101,-5.55717295482336));
#5030=CARTESIAN_POINT('Ctrl Pts',(3.67258562310545,-1.25786066508259,-5.55926892668274));
#5031=CARTESIAN_POINT('Ctrl Pts',(3.55207131652317,-1.26763149215377,-5.56752107953678));
#5032=CARTESIAN_POINT('Ctrl Pts',(3.46190730505992,-1.26531673700144,-5.5737704961506));
#5033=CARTESIAN_POINT('Ctrl Pts',(3.32776485139802,-1.24746938802161,-5.5828114653218));
#5034=CARTESIAN_POINT('Ctrl Pts',(3.28313081164288,-1.23906642879302,-5.58578072864624));
#5035=CARTESIAN_POINT('Ctrl Pts',(3.20590422952255,-1.22017421867164,-5.59085023275138));
#5036=CARTESIAN_POINT('Ctrl Pts',(3.1731073338312,-1.21072985681481,-5.59298144935432));
#5037=CARTESIAN_POINT('Ctrl Pts',(3.09551783294056,-1.18494432674075,-5.59799123775252));
#5038=CARTESIAN_POINT('Ctrl Pts',(3.05118816882779,-1.16737476305348,-5.60082602558441));
#5039=CARTESIAN_POINT('Ctrl Pts',(2.94812926422528,-1.11962730013014,-5.60745846739225));
#5040=CARTESIAN_POINT('Ctrl Pts',(2.89056595536774,-1.08727518220347,-5.61119511748772));
#5041=CARTESIAN_POINT('Ctrl Pts',(2.78830352015497,-1.01877465912023,-5.61825812801595));
#5042=CARTESIAN_POINT('Ctrl Pts',(2.74303612497406,-0.983788655790435,-5.62156687198817));
#5043=CARTESIAN_POINT('Ctrl Pts',(2.6838519083931,-0.931277190323247,-5.62638363008584));
#5044=CARTESIAN_POINT('Ctrl Pts',(2.66779300593776,-0.916262556773373,-5.6277464693398));
#5045=CARTESIAN_POINT('Ctrl Pts',(2.63526749049333,-0.884222773535953,-5.63064569291508));
#5046=CARTESIAN_POINT('Ctrl Pts',(2.61887199637917,-0.867138748811013,-5.63218557213672));
#5047=CARTESIAN_POINT('Ctrl Pts',(2.58341112486266,-0.828048932372558,-5.63567575042531));
#5048=CARTESIAN_POINT('Ctrl Pts',(2.56460649859647,-0.805824236301561,-5.63763806522961));
#5049=CARTESIAN_POINT('Ctrl Pts',(2.4998858357199,-0.723748207857147,-5.64475426343522));
#5050=CARTESIAN_POINT('Ctrl Pts',(2.45857653552093,-0.660464077423448,-5.64999271959722));
#5051=CARTESIAN_POINT('Ctrl Pts',(2.39697872910789,-0.544672047145205,-5.65888001056765));
#5052=CARTESIAN_POINT('Ctrl Pts',(2.37408386428528,-0.493789726746075,-5.66257995845826));
#5053=CARTESIAN_POINT('Ctrl Pts',(2.3425910548086,-0.409279923580441,-5.66838528776535));
#5054=CARTESIAN_POINT('Ctrl Pts',(2.33188615171131,-0.376523359957652,-5.67055834010406));
#5055=CARTESIAN_POINT('Ctrl Pts',(2.31136088024728,-0.303776268951802,-5.67523297503839));
#5056=CARTESIAN_POINT('Ctrl Pts',(2.30212821130146,-0.263660698190303,-5.67771323638318));
#5057=CARTESIAN_POINT('Ctrl Pts',(2.28159558261087,-0.149143516307408,-5.68459356816637));
#5058=CARTESIAN_POINT('Ctrl Pts',(2.27495355791553,-0.0740900462670108,
-5.68886124052725));
#5059=CARTESIAN_POINT('Ctrl Pts',(2.27501953713604,0.00110945800815503,
-5.69316916139296));
#5060=CARTESIAN_POINT('Ctrl Pts',(2.27501952462653,0.00109510754574143,
-5.69341967361942));
#5061=CARTESIAN_POINT('Ctrl Pts',(2.27508084679143,0.0719026266169531,-5.69788243689888));
#5062=CARTESIAN_POINT('Ctrl Pts',(2.28109314086155,0.142459189162486,-5.70234520017833));
#5063=CARTESIAN_POINT('Ctrl Pts',(2.29291052307184,0.211960915112676,-5.70680796345778));
#5064=CARTESIAN_POINT('Ctrl Pts',(2.29497479482244,0.224101543802159,-5.70758752326244));
#5065=CARTESIAN_POINT('Ctrl Pts',(2.29721609154514,0.236210054463847,-5.7083670830671));
#5066=CARTESIAN_POINT('Ctrl Pts',(2.29963349906839,0.248282237669356,-5.70914664287175));
#5067=CARTESIAN_POINT('Ctrl Pts',(2.30931421785275,0.296626345810645,-5.71226845794507));
#5068=CARTESIAN_POINT('Ctrl Pts',(2.321847798193,0.344509128671207,-5.71539027301839));
#5069=CARTESIAN_POINT('Ctrl Pts',(2.33717400774133,0.391569468088145,-5.71851208809171));
#5070=CARTESIAN_POINT('Ctrl Pts',(2.35247223362812,0.438543881457545,-5.7216282031375));
#5071=CARTESIAN_POINT('Ctrl Pts',(2.37055280714682,0.484698312959515,-5.72474431818329));
#5072=CARTESIAN_POINT('Ctrl Pts',(2.3913047909112,0.529683173466743,-5.72786043322908));
#5073=CARTESIAN_POINT('Ctrl Pts',(2.41203589391428,0.574622769957512,-5.73097341282261));
#5074=CARTESIAN_POINT('Ctrl Pts',(2.43543285718586,0.61839463009274,-5.73408639241614));
#5075=CARTESIAN_POINT('Ctrl Pts',(2.46133611263667,0.660667694583638,-5.73719937200966));
#5076=CARTESIAN_POINT('Ctrl Pts',(2.48722431832861,0.702916198477182,-5.74031054296596));
#5077=CARTESIAN_POINT('Ctrl Pts',(2.51561564556851,0.743667165597622,-5.74342171392225));
#5078=CARTESIAN_POINT('Ctrl Pts',(2.54630513890367,0.78261508799952,-5.74653288487854));
#5079=CARTESIAN_POINT('Ctrl Pts',(2.57698985019277,0.821556941524459,-5.74964357105125));
#5080=CARTESIAN_POINT('Ctrl Pts',(2.60997167677727,0.858695878713766,-5.75275425722395));
#5081=CARTESIAN_POINT('Ctrl Pts',(2.64500455080803,0.893758390158439,-5.75586494339665));
#5082=CARTESIAN_POINT('Ctrl Pts',(2.6800715380493,0.928855043673001,-5.75897865859552));
#5083=CARTESIAN_POINT('Ctrl Pts',(2.71719317121231,0.961870847335929,-5.76209237379439));
#5084=CARTESIAN_POINT('Ctrl Pts',(2.75608686802635,0.992569526826832,-5.76520608899327));
#5085=CARTESIAN_POINT('Ctrl Pts',(2.79500178536475,1.02328495561465,-5.76832150304503));
#5086=CARTESIAN_POINT('Ctrl Pts',(2.83569024184058,1.05168042901441,-5.77143691709679));
#5087=CARTESIAN_POINT('Ctrl Pts',(2.87783982272104,1.07756245741384,-5.77455233114855));
#5088=CARTESIAN_POINT('Ctrl Pts',(2.92006688462982,1.10349206318257,-5.77767347207776));
#5089=CARTESIAN_POINT('Ctrl Pts',(2.96375994793821,1.12689874468181,-5.78079461300698));
#5090=CARTESIAN_POINT('Ctrl Pts',(3.00858260762519,1.14763528340201,-5.78391575393619));
#5091=CARTESIAN_POINT('Ctrl Pts',(3.02924435418254,1.1571941340036,-5.78535449548566));
#5092=CARTESIAN_POINT('Ctrl Pts',(3.05014586513611,1.1661862863862,-5.78679323703512));
#5093=CARTESIAN_POINT('Ctrl Pts',(3.07125306164386,1.17460087423461,-5.78823197858459));
#5094=CARTESIAN_POINT('Ctrl Pts',(3.11704109100752,1.19285471459395,-5.79135305344118));
#5095=CARTESIAN_POINT('Ctrl Pts',(3.16399811037257,1.20846708514513,-5.79447412829778));
#5096=CARTESIAN_POINT('Ctrl Pts',(3.21178884403069,1.2212915957371,-5.79759520315438));
#5097=CARTESIAN_POINT('Ctrl Pts',(3.25950731526502,1.23409671490842,-5.80071155876068));
#5098=CARTESIAN_POINT('Ctrl Pts',(3.30805648012053,1.2441221799778,-5.80382791436698));
#5099=CARTESIAN_POINT('Ctrl Pts',(3.3570827507601,1.25127025320884,-5.80694426997328));
#5100=CARTESIAN_POINT('Ctrl Pts',(3.4060557416028,1.25841055819879,-5.81005723884852));
#5101=CARTESIAN_POINT('Ctrl Pts',(3.4555042712478,1.26267958835051,-5.81317020772375));
#5102=CARTESIAN_POINT('Ctrl Pts',(3.50506384158547,1.26403049353406,-5.81628317659899));
#5103=CARTESIAN_POINT('Ctrl Pts',(3.55460065781235,1.26538077848128,-5.8193947162278));
#5104=CARTESIAN_POINT('Ctrl Pts',(3.60424786719166,1.26381557054246,-5.82250625585661));
#5105=CARTESIAN_POINT('Ctrl Pts',(3.65363749481286,1.2593399980347,-5.82561779548543));
#5106=CARTESIAN_POINT('Ctrl Pts',(3.70301483436451,1.25486553904306,-5.82872856096758));
#5107=CARTESIAN_POINT('Ctrl Pts',(3.75213417445898,1.24748220834006,-5.83183932644973));
#5108=CARTESIAN_POINT('Ctrl Pts',(3.80063203620425,1.23724704835227,-5.83495009193188));
#5109=CARTESIAN_POINT('Ctrl Pts',(3.84915605933676,1.22700636717293,-5.83806253546616));
#5110=CARTESIAN_POINT('Ctrl Pts',(3.89705740105416,1.21391090970786,-5.84117497900045));
#5111=CARTESIAN_POINT('Ctrl Pts',(3.9439843271744,1.19806848297683,-5.84428742253473));
#5112=CARTESIAN_POINT('Ctrl Pts',(3.95616735230715,1.19395552056942,-5.84509546561229));
#5113=CARTESIAN_POINT('Ctrl Pts',(3.96828478884944,1.18965766858197,-5.84590350868984));
#5114=CARTESIAN_POINT('Ctrl Pts',(3.98033068509731,1.1851773507521,-5.8467115517674));
#5115=CARTESIAN_POINT('Origin',(3.53951905042299,8.32667268468867E-16,-6.5));
#5116=CARTESIAN_POINT('',(3.98033068509731,1.1851773507521,-6.346783713414));
#5117=CARTESIAN_POINT('',(3.98033068509731,1.1851773507521,-6.20995736687868));
#5118=CARTESIAN_POINT('',(3.98033068509731,1.1851773507521,-6.5));
#5119=CARTESIAN_POINT('',(4.4976352031454,-0.825211298936473,-6.5));
#5120=CARTESIAN_POINT('Ctrl Pts',(3.98033068509731,1.1851773507521,-6.346783713414));
#5121=CARTESIAN_POINT('Ctrl Pts',(4.02616495548084,1.16812987710687,-6.34987250303372));
#5122=CARTESIAN_POINT('Ctrl Pts',(4.07110586500492,1.1483834254578,-6.35296129265343));
#5123=CARTESIAN_POINT('Ctrl Pts',(4.1148117000608,1.12605444685091,-6.35605008227315));
#5124=CARTESIAN_POINT('Ctrl Pts',(4.15843020115214,1.10377008650205,-6.35913269980525));
#5125=CARTESIAN_POINT('Ctrl Pts',(4.20081803353623,1.0789137028647,-6.36221531733735));
#5126=CARTESIAN_POINT('Ctrl Pts',(4.24165368460605,1.05164975418655,-6.36529793486946));
#5127=CARTESIAN_POINT('Ctrl Pts',(4.28245834983294,1.02440649322634,-6.36837821333018));
#5128=CARTESIAN_POINT('Ctrl Pts',(4.32171269959968,0.994759591665204,-6.3714584917909));
#5129=CARTESIAN_POINT('Ctrl Pts',(4.35912171531297,0.962918335948197,-6.37453877025163));
#5130=CARTESIAN_POINT('Ctrl Pts',(4.39651904341382,0.931087028321222,-6.37761808634806));
#5131=CARTESIAN_POINT('Ctrl Pts',(4.43207175366471,0.897063087696465,-6.3806974024445));
#5132=CARTESIAN_POINT('Ctrl Pts',(4.46551781507142,0.86109612580105,-6.38377671854093));
#5133=CARTESIAN_POINT('Ctrl Pts',(4.49913236819104,0.824947972615459,-6.38687154735312));
#5134=CARTESIAN_POINT('Ctrl Pts',(4.5306185831317,0.786837569042,-6.3899663761653));
#5135=CARTESIAN_POINT('Ctrl Pts',(4.55974993405299,0.747053675506357,-6.39306120497749));
#5136=CARTESIAN_POINT('Ctrl Pts',(4.58877680192034,0.70741247163537,-6.39614493381815));
#5137=CARTESIAN_POINT('Ctrl Pts',(4.61546539872469,0.666110259798259,-6.39922866265882));
#5138=CARTESIAN_POINT('Ctrl Pts',(4.63963574546676,0.623460910792302,-6.40231239149948));
#5139=CARTESIAN_POINT('Ctrl Pts',(4.66393659500647,0.580581285430692,-6.40541277029743));
#5140=CARTESIAN_POINT('Ctrl Pts',(4.68569167562811,0.536340448700378,-6.40851314909538));
#5141=CARTESIAN_POINT('Ctrl Pts',(4.70476677812757,0.49107838791715,-6.41161352789333));
#5142=CARTESIAN_POINT('Ctrl Pts',(4.72384188062704,0.445816327133923,-6.41471390669127));
#5143=CARTESIAN_POINT('Ctrl Pts',(4.74023689245796,0.399533602083208,-6.41781428548922));
#5144=CARTESIAN_POINT('Ctrl Pts',(4.75386885489192,0.352583043248368,-6.42091466428717));
#5145=CARTESIAN_POINT('Ctrl Pts',(4.76835751896294,0.302681873244369,-6.42420988660854));
#5146=CARTESIAN_POINT('Ctrl Pts',(4.77979240021909,0.251794251730069,-6.42750510892991));
#5147=CARTESIAN_POINT('Ctrl Pts',(4.78805146309887,0.200317409372577,-6.43080033125128));
#5148=CARTESIAN_POINT('Ctrl Pts',(4.79607098831799,0.150333550247694,-6.43399998221574));
#5149=CARTESIAN_POINT('Ctrl Pts',(4.8010963166219,0.0997947297249169,-6.43719963318019));
#5150=CARTESIAN_POINT('Ctrl Pts',(4.80306622942805,0.0490792871622248,-6.44039928414465));
#5151=CARTESIAN_POINT('Ctrl Pts',(4.80503359056896,-0.00157046273056229,
-6.44359479054083));
#5152=CARTESIAN_POINT('Ctrl Pts',(4.80395336896427,-0.0523958723376958,
-6.44679029693701));
#5153=CARTESIAN_POINT('Ctrl Pts',(4.79981605772876,-0.103013122349091,-6.44998580333318));
#5154=CARTESIAN_POINT('Ctrl Pts',(4.79568270901791,-0.153581893508067,-6.45317824922167));
#5155=CARTESIAN_POINT('Ctrl Pts',(4.78849812398825,-0.20394239251437,-6.45637069511015));
#5156=CARTESIAN_POINT('Ctrl Pts',(4.778304816312,-0.253712585873823,-6.45956314099864));
#5157=CARTESIAN_POINT('Ctrl Pts',(4.76811783502728,-0.303451889777174,-6.46275360552217));
#5158=CARTESIAN_POINT('Ctrl Pts',(4.75492594267193,-0.352601115387661,-6.46594407004569));
#5159=CARTESIAN_POINT('Ctrl Pts',(4.73882294389742,-0.400787251664849,-6.46913453456922));
#5160=CARTESIAN_POINT('Ctrl Pts',(4.72271981198959,-0.448973786326264,-6.47232502547027));
#5161=CARTESIAN_POINT('Ctrl Pts',(4.70370567730319,-0.496196727080413,-6.47551551637131));
#5162=CARTESIAN_POINT('Ctrl Pts',(4.68192401564236,-0.542098833647634,-6.47870600727236));
#5163=CARTESIAN_POINT('Ctrl Pts',(4.66014245444853,-0.588000728493317,-6.4818964834574));
#5164=CARTESIAN_POINT('Ctrl Pts',(4.63559361893804,-0.632581342776674,-6.48508695964244));
#5165=CARTESIAN_POINT('Ctrl Pts',(4.6084678042507,-0.675506337268713,-6.48827743582748));
#5166=CARTESIAN_POINT('Ctrl Pts',(4.58132277162687,-0.718461743006546,-6.49147017238218));
#5167=CARTESIAN_POINT('Ctrl Pts',(4.55159739891111,-0.7597587613696,-6.49466290893689));
#5168=CARTESIAN_POINT('Ctrl Pts',(4.51952538136017,-0.799091885406837,-6.4978556454916));
#5169=CARTESIAN_POINT('Ctrl Pts',(4.5123451485358,-0.807897723326088,-6.49857043032773));
#5170=CARTESIAN_POINT('Ctrl Pts',(4.50504745829283,-0.816605259011897,-6.49928521516387));
#5171=CARTESIAN_POINT('Ctrl Pts',(4.49763520314539,-0.825211298936477,-6.5));
#5172=CARTESIAN_POINT('',(2.58129066896548,-0.825080977219403,-6.49999893616038));
#5173=CARTESIAN_POINT('Origin',(3.53951905042299,8.32667268468867E-16,-6.5));
#5174=CARTESIAN_POINT('Ctrl Pts',(2.58129066896548,-0.825080977219403,-6.49999893616038));
#5175=CARTESIAN_POINT('Ctrl Pts',(2.61412671854531,-0.863215942769539,-6.49681298227165));
#5176=CARTESIAN_POINT('Ctrl Pts',(2.64931926798332,-0.899476323465664,-6.49362702838292));
#5177=CARTESIAN_POINT('Ctrl Pts',(2.68662301217427,-0.933556960200953,-6.49044107449419));
#5178=CARTESIAN_POINT('Ctrl Pts',(2.72294455751986,-0.966740261755096,-6.48733900602497));
#5179=CARTESIAN_POINT('Ctrl Pts',(2.7612670549967,-0.997856790145826,-6.48423693755575));
#5180=CARTESIAN_POINT('Ctrl Pts',(2.80132380814607,-1.02665867467222,-6.48113486908654));
#5181=CARTESIAN_POINT('Ctrl Pts',(2.84134145438787,-1.05543244027864,-6.478035829128));
#5182=CARTESIAN_POINT('Ctrl Pts',(2.88308955800233,-1.08189571288545,-6.47493678916947));
#5183=CARTESIAN_POINT('Ctrl Pts',(2.92626824205562,-1.10584071910776,-6.47183774921094));
#5184=CARTESIAN_POINT('Ctrl Pts',(2.96942356684567,-1.12977277130621,-6.46874038580397));
#5185=CARTESIAN_POINT('Ctrl Pts',(3.01400745582359,-1.15118898787877,-6.465643022397));
#5186=CARTESIAN_POINT('Ctrl Pts',(3.05969320088253,-1.16992623874874,-6.46254565899003));
#5187=CARTESIAN_POINT('Ctrl Pts',(3.10764213745995,-1.18959170009648,-6.45929485764343));
#5188=CARTESIAN_POINT('Ctrl Pts',(3.1568043809889,-1.20630549959918,-6.45604405629683));
#5189=CARTESIAN_POINT('Ctrl Pts',(3.20677870465072,-1.21993610992353,-6.45279325495023));
#5190=CARTESIAN_POINT('Ctrl Pts',(3.2544370462731,-1.23293503088453,-6.44969310691879));
#5191=CARTESIAN_POINT('Ctrl Pts',(3.30283326198768,-1.24313020620206,-6.44659295888735));
#5192=CARTESIAN_POINT('Ctrl Pts',(3.35160723959285,-1.2504596760194,-6.44349281085591));
#5193=CARTESIAN_POINT('Ctrl Pts',(3.4004119123784,-1.25779375853,-6.44039071179223));
#5194=CARTESIAN_POINT('Ctrl Pts',(3.44959426890379,-1.2622584995746,-6.43728861272854));
#5195=CARTESIAN_POINT('Ctrl Pts',(3.49879002678772,-1.26384389725698,-6.43418651366486));
#5196=CARTESIAN_POINT('Ctrl Pts',(3.54806997554175,-1.26543200810034,-6.43107910584224));
#5197=CARTESIAN_POINT('Ctrl Pts',(3.59736281976622,-1.26413097060597,-6.42797169801961));
#5198=CARTESIAN_POINT('Ctrl Pts',(3.64630722476824,-1.25998275219148,-6.42486429019699));
#5199=CARTESIAN_POINT('Ctrl Pts',(3.65328091267178,-1.25939170648202,-6.42442154107494));
#5200=CARTESIAN_POINT('Ctrl Pts',(3.66024754291994,-1.25874294487555,-6.42397879195289));
#5201=CARTESIAN_POINT('Ctrl Pts',(3.66720608834692,-1.258036672894,-6.42353604283084));
#5202=CARTESIAN_POINT('Ctrl Pts',(3.7163503009999,-1.25304867923693,-6.42040915988751));
#5203=CARTESIAN_POINT('Ctrl Pts',(3.76530520024984,-1.24516622469272,-6.41728227694418));
#5204=CARTESIAN_POINT('Ctrl Pts',(3.81370450644581,-1.23441588846934,-6.41415539400084));
#5205=CARTESIAN_POINT('Ctrl Pts',(3.86201822470779,-1.22368456282978,-6.41103404054692));
#5206=CARTESIAN_POINT('Ctrl Pts',(3.90977776996751,-1.21009553271363,-6.40791268709299));
#5207=CARTESIAN_POINT('Ctrl Pts',(3.95662365314126,-1.19372693711386,-6.40479133363907));
#5208=CARTESIAN_POINT('Ctrl Pts',(4.00342399311994,-1.17737425493255,-6.40167301474015));
#5209=CARTESIAN_POINT('Ctrl Pts',(4.04931191683946,-1.15824753723455,-6.39855469584123));
#5210=CARTESIAN_POINT('Ctrl Pts',(4.09394188046512,-1.13647506595089,-6.39543637694231));
#5211=CARTESIAN_POINT('Ctrl Pts',(4.13854724887414,-1.11471459330232,-6.39231977652404));
#5212=CARTESIAN_POINT('Ctrl Pts',(4.18189554117391,-1.09031149514611,-6.38920317610577));
#5213=CARTESIAN_POINT('Ctrl Pts',(4.22366242409282,-1.06344162710685,-6.3860865756875));
#5214=CARTESIAN_POINT('Ctrl Pts',(4.26542387626861,-1.03657525282487,-6.38297038050551));
#5215=CARTESIAN_POINT('Ctrl Pts',(4.30560386937867,-1.00724304192177,-6.37985418532352));
#5216=CARTESIAN_POINT('Ctrl Pts',(4.34390607352076,-0.975664782121349,-6.37673799014153));
#5217=CARTESIAN_POINT('Ctrl Pts',(4.3822464430242,-0.944055056881205,-6.37361868989764));
#5218=CARTESIAN_POINT('Ctrl Pts',(4.41870486724809,-0.91019516380421,-6.37049938965374));
#5219=CARTESIAN_POINT('Ctrl Pts',(4.45301863913752,-0.874344755470276,-6.36738008940984));
#5220=CARTESIAN_POINT('Ctrl Pts',(4.48735166185403,-0.838474234220356,-6.36425903916568));
#5221=CARTESIAN_POINT('Ctrl Pts',(4.5195372825782,-0.800611390248026,-6.36113798892153));
#5222=CARTESIAN_POINT('Ctrl Pts',(4.54935255743518,-0.761049629206565,-6.35801693867737));
#5223=CARTESIAN_POINT('Ctrl Pts',(4.57922266965563,-0.721415104701414,-6.35489014808142));
#5224=CARTESIAN_POINT('Ctrl Pts',(4.60671343338299,-0.680075881820579,-6.35176335748547));
#5225=CARTESIAN_POINT('Ctrl Pts',(4.63164568014743,-0.637353649590818,-6.34863656688951));
#5226=CARTESIAN_POINT('Ctrl Pts',(4.64277134670996,-0.618289450720728,-6.34724128029902));
#5227=CARTESIAN_POINT('Ctrl Pts',(4.65338816691601,-0.598950168489519,-6.34584599370852));
#5228=CARTESIAN_POINT('Ctrl Pts',(4.66348329935251,-0.579365702409359,-6.34445070711802));
#5229=CARTESIAN_POINT('Ctrl Pts',(4.68604213954088,-0.535601755452205,-6.34133276414798));
#5230=CARTESIAN_POINT('Ctrl Pts',(4.70609159237177,-0.490420275785111,-6.33821482117794));
#5231=CARTESIAN_POINT('Ctrl Pts',(4.72345315202669,-0.444139947606419,-6.3350968782079));
#5232=CARTESIAN_POINT('Ctrl Pts',(4.74078251756512,-0.397945438576851,-6.33198471694303));
#5233=CARTESIAN_POINT('Ctrl Pts',(4.75543368336745,-0.350656632335413,-6.32887255567816));
#5234=CARTESIAN_POINT('Ctrl Pts',(4.76727490792033,-0.302614944080707,-6.32576039441329));
#5235=CARTESIAN_POINT('Ctrl Pts',(4.77910402283558,-0.254622386507843,-6.32265141585516));
#5236=CARTESIAN_POINT('Ctrl Pts',(4.78812875400986,-0.205879001956756,-6.31954243729703));
#5237=CARTESIAN_POINT('Ctrl Pts',(4.79426689094177,-0.15674216635436,-6.31643345873889));
#5238=CARTESIAN_POINT('Ctrl Pts',(4.80040137886605,-0.107634541681869,-6.31332632841038));
#5239=CARTESIAN_POINT('Ctrl Pts',(4.80365260386734,-0.0581344735108271,
-6.31021919808186));
#5240=CARTESIAN_POINT('Ctrl Pts',(4.80398975244913,-0.00860777076329439,
-6.30711206775334));
#5241=CARTESIAN_POINT('Ctrl Pts',(4.8043268449561,0.0409106946627478,-6.30400545420527));
#5242=CARTESIAN_POINT('Ctrl Pts',(4.80175082049702,0.0904552366909444,-6.3008988406572));
#5243=CARTESIAN_POINT('Ctrl Pts',(4.7962829578317,0.139659339232284,-6.29779222710913));
#5244=CARTESIAN_POINT('Ctrl Pts',(4.79080979264191,0.188911158033825,-6.29468260088583));
#5245=CARTESIAN_POINT('Ctrl Pts',(4.78243925225903,0.237821331195318,-6.29157297466254));
#5246=CARTESIAN_POINT('Ctrl Pts',(4.77124438860737,0.286029616079496,-6.28846334843925));
#5247=CARTESIAN_POINT('Ctrl Pts',(4.76004346383081,0.334264001901106,-6.28535203860162));
#5248=CARTESIAN_POINT('Ctrl Pts',(4.74601532686642,0.381795215322045,-6.282240728764));
#5249=CARTESIAN_POINT('Ctrl Pts',(4.72928304450845,0.42827781681733,-6.27912941892637));
#5250=CARTESIAN_POINT('Ctrl Pts',(4.71251983522219,0.474846333912903,-6.27601235833376));
#5251=CARTESIAN_POINT('Ctrl Pts',(4.69304272248403,0.520361865968394,-6.27289529774114));
#5252=CARTESIAN_POINT('Ctrl Pts',(4.67102239639318,0.564500157713225,-6.26977823714853));
#5253=CARTESIAN_POINT('Ctrl Pts',(4.66063090310688,0.585329220845309,-6.26830728190075));
#5254=CARTESIAN_POINT('Ctrl Pts',(4.64967370496905,0.605851960151309,-6.26683632665297));
#5255=CARTESIAN_POINT('Ctrl Pts',(4.63817208739712,0.626036543939347,-6.26536537140519));
#5256=CARTESIAN_POINT('Ctrl Pts',(4.61376229710427,0.668874123465282,-6.26224357493579));
#5257=CARTESIAN_POINT('Ctrl Pts',(4.58679013796971,0.710375291807168,-6.25912177846638));
#5258=CARTESIAN_POINT('Ctrl Pts',(4.55742651536473,0.750216397325387,-6.25599998199698));
#5259=CARTESIAN_POINT('Ctrl Pts',(4.52810762303525,0.789996811979615,-6.25288294103129));
#5260=CARTESIAN_POINT('Ctrl Pts',(4.49640480327601,0.82812173430381,-6.24976590006559));
#5261=CARTESIAN_POINT('Ctrl Pts',(4.46253361238668,0.864294144607594,-6.24664885909989));
#5262=CARTESIAN_POINT('Ctrl Pts',(4.42869624467415,0.900430433777259,-6.2435349307566));
#5263=CARTESIAN_POINT('Ctrl Pts',(4.39269516505254,0.934617672677172,-6.24042100241331));
#5264=CARTESIAN_POINT('Ctrl Pts',(4.35478626440368,0.966591754469368,-6.23730707407002));
#5265=CARTESIAN_POINT('Ctrl Pts',(4.31690142905875,0.998545538495526,-6.23419512250872));
#5266=CARTESIAN_POINT('Ctrl Pts',(4.27711159225709,1.02828859884005,-6.23108317094741));
#5267=CARTESIAN_POINT('Ctrl Pts',(4.235707637073,1.05559542525452,-6.22797121938611));
#5268=CARTESIAN_POINT('Ctrl Pts',(4.19428956444941,1.08291156243333,-6.22485820674773));
#5269=CARTESIAN_POINT('Ctrl Pts',(4.15125672490063,1.10778949401323,-6.22174519410934));
#5270=CARTESIAN_POINT('Ctrl Pts',(4.10692943142985,1.13004677315838,-6.21863218147096));
#5271=CARTESIAN_POINT('Ctrl Pts',(4.06575484195602,1.1507210408578,-6.21574057660687));
#5272=CARTESIAN_POINT('Ctrl Pts',(4.0234639866436,1.16913446809706,-6.21284897174278));
#5273=CARTESIAN_POINT('Ctrl Pts',(3.98033068509731,1.1851773507521,-6.20995736687868));
#5274=CARTESIAN_POINT('Origin',(3.53951905042299,8.32667268468867E-16,-6.5));
#5275=CARTESIAN_POINT('',(2.27501933211556,-0.00084403816866925,-6.05658032632122));
#5276=CARTESIAN_POINT('Ctrl Pts',(3.98033068509731,1.1851773507521,-6.20995736687868));
#5277=CARTESIAN_POINT('Ctrl Pts',(3.93385133118698,1.20246475500667,-6.20684144667251));
#5278=CARTESIAN_POINT('Ctrl Pts',(3.88639406205051,1.21699885353846,-6.20372552646634));
#5279=CARTESIAN_POINT('Ctrl Pts',(3.83831564831889,1.22869070277505,-6.20060960626016));
#5280=CARTESIAN_POINT('Ctrl Pts',(3.79014801406301,1.24040424891961,-6.19748790374936));
#5281=CARTESIAN_POINT('Ctrl Pts',(3.7413574735584,1.24926491911046,-6.19436620123856));
#5282=CARTESIAN_POINT('Ctrl Pts',(3.69230960462601,1.25523515587572,-6.19124449872775));
#5283=CARTESIAN_POINT('Ctrl Pts',(3.66630922700763,1.25839999083688,-6.18958967771596));
#5284=CARTESIAN_POINT('Ctrl Pts',(3.64023660268906,1.26075347117176,-6.18793485670416));
#5285=CARTESIAN_POINT('Ctrl Pts',(3.61414616017263,1.26229594172302,-6.18628003569237));
#5286=CARTESIAN_POINT('Ctrl Pts',(3.56491893879061,1.26520626182413,-6.18315773371363));
#5287=CARTESIAN_POINT('Ctrl Pts',(3.51541402755449,1.26523895392596,-6.18003543173489));
#5288=CARTESIAN_POINT('Ctrl Pts',(3.4659961307317,1.26236073698451,-6.17691312975614));
#5289=CARTESIAN_POINT('Ctrl Pts',(3.41666811577358,1.25948775497862,-6.17379650665777));
#5290=CARTESIAN_POINT('Ctrl Pts',(3.36742734378295,1.25371439647113,-6.17067988355939));
#5291=CARTESIAN_POINT('Ctrl Pts',(3.31864021813992,1.24505935258094,-6.16756326046101));
#5292=CARTESIAN_POINT('Ctrl Pts',(3.26990197615981,1.23641298086076,-6.16444976015274));
#5293=CARTESIAN_POINT('Ctrl Pts',(3.22161701740165,1.22489073538295,-6.16133625984446));
#5294=CARTESIAN_POINT('Ctrl Pts',(3.17414614658414,1.21056304715631,-6.15822275953619));
#5295=CARTESIAN_POINT('Ctrl Pts',(3.12670267433917,1.19624362838414,-6.15511105623442));
#5296=CARTESIAN_POINT('Ctrl Pts',(3.08007288253499,1.1791221328155,-6.15199935293266));
#5297=CARTESIAN_POINT('Ctrl Pts',(3.0346043656427,1.15931937406964,-6.1488876496309));
#5298=CARTESIAN_POINT('Ctrl Pts',(2.989142777331,1.13951963290648,-6.1457764204965));
#5299=CARTESIAN_POINT('Ctrl Pts',(2.94484261399633,1.11703965943637,-6.14266519136211));
#5300=CARTESIAN_POINT('Ctrl Pts',(2.90203094213092,1.09204814993946,-6.13955396222772));
#5301=CARTESIAN_POINT('Ctrl Pts',(2.85917742828406,1.06703221499427,-6.13643969233397));
#5302=CARTESIAN_POINT('Ctrl Pts',(2.81781578352711,1.03950012118479,-6.13332542244023));
#5303=CARTESIAN_POINT('Ctrl Pts',(2.77824631821777,1.00966532930511,-6.13021115254648));
#5304=CARTESIAN_POINT('Ctrl Pts',(2.73865517234765,0.979814190603118,-6.12709517630878));
#5305=CARTESIAN_POINT('Ctrl Pts',(2.70085857873599,0.947658196795133,-6.12397920007109));
#5306=CARTESIAN_POINT('Ctrl Pts',(2.66512302989052,0.913450518242225,-6.12086322383339));
#5307=CARTESIAN_POINT('Ctrl Pts',(2.62932174457812,0.879179913779319,-6.11774151567676));
#5308=CARTESIAN_POINT('Ctrl Pts',(2.5955894429348,0.842850494239972,-6.11461980752013));
#5309=CARTESIAN_POINT('Ctrl Pts',(2.56415394704208,0.804750374406088,-6.11149809936351));
#5310=CARTESIAN_POINT('Ctrl Pts',(2.54970891813782,0.787242862066077,-6.11006363290218));
#5311=CARTESIAN_POINT('Ctrl Pts',(2.53574827647228,0.769361887651816,-6.10862916644086));
#5312=CARTESIAN_POINT('Ctrl Pts',(2.52229100852905,0.751137378103785,-6.10719469997954));
#5313=CARTESIAN_POINT('Ctrl Pts',(2.49287301930624,0.71129805650176,-6.10405891349764));
#5314=CARTESIAN_POINT('Ctrl Pts',(2.4657340203538,0.669640051077935,-6.10092312701574));
#5315=CARTESIAN_POINT('Ctrl Pts',(2.4411031690058,0.626452553231681,-6.09778734053384));
#5316=CARTESIAN_POINT('Ctrl Pts',(2.41651339891891,0.583337086873545,-6.094656784162));
#5317=CARTESIAN_POINT('Ctrl Pts',(2.3944237547299,0.538697647781062,-6.09152622779015));
#5318=CARTESIAN_POINT('Ctrl Pts',(2.37502105402754,0.492853595290712,-6.08839567141831));
#5319=CARTESIAN_POINT('Ctrl Pts',(2.35564416242351,0.44707052367499,-6.08526927925219));
#5320=CARTESIAN_POINT('Ctrl Pts',(2.33894733547462,0.400086512493713,-6.08214288708606));
#5321=CARTESIAN_POINT('Ctrl Pts',(2.32507100364992,0.352244505548458,-6.07901649491994));
#5322=CARTESIAN_POINT('Ctrl Pts',(2.3112053781611,0.304439411283135,-6.07589251493342));
#5323=CARTESIAN_POINT('Ctrl Pts',(2.30015608341166,0.255778152169922,-6.0727685349469));
#5324=CARTESIAN_POINT('Ctrl Pts',(2.29201423199374,0.206620371686356,-6.06964455496038));
#5325=CARTESIAN_POINT('Ctrl Pts',(2.28387383969977,0.157471400906018,-6.06652113483105));
#5326=CARTESIAN_POINT('Ctrl Pts',(2.27863995220415,0.107826617675868,-6.06339771470171));
#5327=CARTESIAN_POINT('Ctrl Pts',(2.27635245514721,0.0580551684123632,-6.06027429457238));
#5328=CARTESIAN_POINT('Ctrl Pts',(2.27545067216389,0.038434139452019,-6.05904297184178));
#5329=CARTESIAN_POINT('Ctrl Pts',(2.27500622432079,0.0187934877093903,-6.05781164911118));
#5330=CARTESIAN_POINT('Ctrl Pts',(2.27501933211493,-0.000844037222033078,
-6.05658032638058));
#5331=CARTESIAN_POINT('Ctrl Pts',(2.27501933211556,-0.000844038168669184,
-6.05658032632122));
#5332=CARTESIAN_POINT('Ctrl Pts',(2.27505698654879,-0.0572562029046497,
-6.05304314019587));
#5333=CARTESIAN_POINT('Ctrl Pts',(2.27887371445784,-0.113521864639994,-6.04950595407052));
#5334=CARTESIAN_POINT('Ctrl Pts',(2.2863868355746,-0.16917417683907,-6.04596876794517));
#5335=CARTESIAN_POINT('Ctrl Pts',(2.29396582199884,-0.225314376375244,-6.04240057235675));
#5336=CARTESIAN_POINT('Ctrl Pts',(2.30530616689083,-0.280830190252909,-6.03883237676834));
#5337=CARTESIAN_POINT('Ctrl Pts',(2.32027339706781,-0.335261519972844,-6.03526418117992));
#5338=CARTESIAN_POINT('Ctrl Pts',(2.3302773135162,-0.371642765417343,-6.03287924220886));
#5339=CARTESIAN_POINT('Ctrl Pts',(2.34190049367822,-0.407539927551625,-6.03049430323779));
#5340=CARTESIAN_POINT('Ctrl Pts',(2.35509102814013,-0.442821081285782,-6.02810936426672));
#5341=CARTESIAN_POINT('Ctrl Pts',(2.3723573653824,-0.489003917957764,-6.02498749223829));
#5342=CARTESIAN_POINT('Ctrl Pts',(2.39236660219172,-0.534276316559383,-6.02186562020986));
#5343=CARTESIAN_POINT('Ctrl Pts',(2.41500167232912,-0.578291376699397,-6.01874374818142));
#5344=CARTESIAN_POINT('Ctrl Pts',(2.43759542894926,-0.622226100576454,-6.01562757419206));
#5345=CARTESIAN_POINT('Ctrl Pts',(2.46280526458397,-0.66490755431047,-6.01251140020269));
#5346=CARTESIAN_POINT('Ctrl Pts',(2.4904658960776,-0.706008306861882,-6.00939522621333));
#5347=CARTESIAN_POINT('Ctrl Pts',(2.51809870624658,-0.747067719887846,-6.00628218650122));
#5348=CARTESIAN_POINT('Ctrl Pts',(2.54817712765057,-0.786549126907373,-6.00316914678911));
#5349=CARTESIAN_POINT('Ctrl Pts',(2.58049082464027,-0.824151146424035,-6.000056107077));
#5350=CARTESIAN_POINT('Ctrl Pts',(2.61278575862353,-0.861731332260242,-5.99694487495701));
#5351=CARTESIAN_POINT('Ctrl Pts',(2.64731304035497,-0.897433877815161,-5.99383364283702));
#5352=CARTESIAN_POINT('Ctrl Pts',(2.68382160328835,-0.930989865125965,-5.99072241071704));
#5353=CARTESIAN_POINT('Ctrl Pts',(2.72032448831636,-0.964540633723522,-5.98761166246385));
#5354=CARTESIAN_POINT('Ctrl Pts',(2.75880763883495,-0.995945137171808,-5.98450091421067));
#5355=CARTESIAN_POINT('Ctrl Pts',(2.79898450572692,-1.02497260359084,-5.98139016595749));
#5356=CARTESIAN_POINT('Ctrl Pts',(2.83920050514222,-1.05402834294638,-5.97827638781576));
#5357=CARTESIAN_POINT('Ctrl Pts',(2.88111306881727,-1.08070210253111,-5.97516260967404));
#5358=CARTESIAN_POINT('Ctrl Pts',(2.92440553907012,-1.10480569248676,-5.97204883153231));
#5359=CARTESIAN_POINT('Ctrl Pts',(2.96772163741902,-1.12892243766167,-5.96893335395767));
#5360=CARTESIAN_POINT('Ctrl Pts',(3.01241864799431,-1.15046598192878,-5.96581787638303));
#5361=CARTESIAN_POINT('Ctrl Pts',(3.05815728581959,-1.16929513022928,-5.96270239880838));
#5362=CARTESIAN_POINT('Ctrl Pts',(3.10398000247744,-1.18815889112172,-5.95958119422197));
#5363=CARTESIAN_POINT('Ctrl Pts',(3.15084764941867,-1.20429811992803,-5.95645998963555));
#5364=CARTESIAN_POINT('Ctrl Pts',(3.19840463755624,-1.2176211263503,-5.95333878504913));
#5365=CARTESIAN_POINT('Ctrl Pts',(3.22031891432334,-1.22376037236947,-5.95190053288405));
#5366=CARTESIAN_POINT('Ctrl Pts',(3.24237941204166,-1.22930234408423,-5.95046228071898));
#5367=CARTESIAN_POINT('Ctrl Pts',(3.26455079222824,-1.23424175386564,-5.9490240285539));
#5368=CARTESIAN_POINT('Ctrl Pts',(3.31267501798266,-1.24496302017447,-5.94590222146288));
#5369=CARTESIAN_POINT('Ctrl Pts',(3.36153242312082,-1.2528888973427,-5.94278041437187));
#5370=CARTESIAN_POINT('Ctrl Pts',(3.41076841946522,-1.25792826704386,-5.93965860728085));
#5371=CARTESIAN_POINT('Ctrl Pts',(3.45991456907007,-1.26295844081175,-5.93654249692006));
#5372=CARTESIAN_POINT('Ctrl Pts',(3.5094373989117,-1.26511249897277,-5.93342638655928));
#5373=CARTESIAN_POINT('Ctrl Pts',(3.55897233558323,-1.26435035480537,-5.93031027619849));
#5374=CARTESIAN_POINT('Ctrl Pts',(3.6084574623759,-1.2635889770124,-5.92719729924394));
#5375=CARTESIAN_POINT('Ctrl Pts',(3.6579541266216,-1.25991721067633,-5.92408432228939));
#5376=CARTESIAN_POINT('Ctrl Pts',(3.7070950113436,-1.25334693813067,-5.92097134533484));
#5377=CARTESIAN_POINT('Ctrl Pts',(3.75620737743784,-1.24678047860463,-5.91786017497843));
#5378=CARTESIAN_POINT('Ctrl Pts',(3.80496383097999,-1.23731891793616,-5.91474900462202));
#5379=CARTESIAN_POINT('Ctrl Pts',(3.85300204483451,-1.22502598430188,-5.91163783426561));
#5380=CARTESIAN_POINT('Ctrl Pts',(3.90103280477825,-1.21273495811634,-5.90852714665792));
#5381=CARTESIAN_POINT('Ctrl Pts',(3.9483450160688,-1.19761356809752,-5.90541645905024));
#5382=CARTESIAN_POINT('Ctrl Pts',(3.994588967302,-1.17977608924394,-5.90230577144255));
#5383=CARTESIAN_POINT('Ctrl Pts',(4.04087799371517,-1.16192122373658,-5.89919205176688));
#5384=CARTESIAN_POINT('Ctrl Pts',(4.08609616954537,-1.14134518260638,-5.89607833209122));
#5385=CARTESIAN_POINT('Ctrl Pts',(4.12991304844692,-1.11821070335483,-5.89296461241555));
#5386=CARTESIAN_POINT('Ctrl Pts',(4.17375385850482,-1.09506358890759,-5.88984919214153));
#5387=CARTESIAN_POINT('Ctrl Pts',(4.21619137863636,-1.06935553811172,-5.8867337718675));
#5388=CARTESIAN_POINT('Ctrl Pts',(4.25692220755705,-1.04129388749482,-5.88361835159347));
#5389=CARTESIAN_POINT('Ctrl Pts',(4.2977279433308,-1.01318062953295,-5.88049720184291));
#5390=CARTESIAN_POINT('Ctrl Pts',(4.33682029192501,-0.982705470712209,-5.87737605209235));
#5391=CARTESIAN_POINT('Ctrl Pts',(4.37392844987612,-0.950116416079766,-5.87425490234178));
#5392=CARTESIAN_POINT('Ctrl Pts',(4.39103396084727,-0.935094047351874,-5.87281616584154));
#5393=CARTESIAN_POINT('Ctrl Pts',(4.40771837197739,-0.919623019014169,-5.87137742934131));
#5394=CARTESIAN_POINT('Ctrl Pts',(4.42395795142166,-0.903730092671621,-5.86993869284107));
#5395=CARTESIAN_POINT('Ctrl Pts',(4.45919242271407,-0.869247742996835,-5.86681711447206));
#5396=CARTESIAN_POINT('Ctrl Pts',(4.49248440852953,-0.83262626144501,-5.86369553610306));
#5397=CARTESIAN_POINT('Ctrl Pts',(4.52356411872374,-0.794113060938407,-5.86057395773406));
#5398=CARTESIAN_POINT('Ctrl Pts',(4.55458706730217,-0.755670198008187,-5.85745808037806));
#5399=CARTESIAN_POINT('Ctrl Pts',(4.58340541236112,-0.715342891540266,-5.85434220302206));
#5400=CARTESIAN_POINT('Ctrl Pts',(4.60978668200981,-0.673414765785208,-5.85122632566606));
#5401=CARTESIAN_POINT('Ctrl Pts',(4.6361414012232,-0.631528837013262,-5.84811358416748));
#5402=CARTESIAN_POINT('Ctrl Pts',(4.66006361025982,-0.588045740121642,-5.8450008426689));
#5403=CARTESIAN_POINT('Ctrl Pts',(4.68136289272615,-0.543279752792577,-5.84188810117032));
#5404=CARTESIAN_POINT('Ctrl Pts',(4.70264979966691,-0.498539775852419,-5.83877716826843));
#5405=CARTESIAN_POINT('Ctrl Pts',(4.72131656430274,-0.452518879168679,-5.83566623536655));
#5406=CARTESIAN_POINT('Ctrl Pts',(4.73721894244515,-0.405555444606648,-5.83255530246467));
#5407=CARTESIAN_POINT('Ctrl Pts',(4.75311884496686,-0.358599321130413,-5.82944485386079));
#5408=CARTESIAN_POINT('Ctrl Pts',(4.76625504083263,-0.310701470233705,-5.82633440525691));
#5409=CARTESIAN_POINT('Ctrl Pts',(4.77653253037065,-0.262217277134401,-5.82322395665302));
#5410=CARTESIAN_POINT('Ctrl Pts',(4.78682003688283,-0.213685828826787,-5.82011047644467));
#5411=CARTESIAN_POINT('Ctrl Pts',(4.79424316182307,-0.164567434723309,-5.81699699623631));
#5412=CARTESIAN_POINT('Ctrl Pts',(4.79875803108361,-0.115227772627966,-5.81388351602795));
#5413=CARTESIAN_POINT('Ctrl Pts',(4.80327536551357,-0.0658611705219124,
-5.81076833582437));
#5414=CARTESIAN_POINT('Ctrl Pts',(4.80488126460168,-0.0162736080643454,
-5.80765315562078));
#5415=CARTESIAN_POINT('Ctrl Pts',(4.8035839862753,0.0331675737536573,-5.80453797541719));
#5416=CARTESIAN_POINT('Ctrl Pts',(4.80228432121647,0.0826997174496432,-5.80141706390559));
#5417=CARTESIAN_POINT('Ctrl Pts',(4.79807086613848,0.13208439691815,-5.79829615239399));
#5418=CARTESIAN_POINT('Ctrl Pts',(4.79100374597293,0.180959406509492,-5.79517524088239));
#5419=CARTESIAN_POINT('Ctrl Pts',(4.78774152896586,0.203520348417172,-5.79373461296434));
#5420=CARTESIAN_POINT('Ctrl Pts',(4.78387197165841,0.225972841006474,-5.7922939850463));
#5421=CARTESIAN_POINT('Ctrl Pts',(4.7794045979522,0.248282256772818,-5.79085335712825));
#5422=CARTESIAN_POINT('Ctrl Pts',(4.76972387646597,0.296626374537997,-5.78773154136868));
#5423=CARTESIAN_POINT('Ctrl Pts',(4.75719029232652,0.344509166555588,-5.78460972560912));
#5424=CARTESIAN_POINT('Ctrl Pts',(4.74186407797352,0.391569514549487,-5.78148790984956));
#5425=CARTESIAN_POINT('Ctrl Pts',(4.7265658473038,0.438543936440369,-5.77837179412143));
#5426=CARTESIAN_POINT('Ctrl Pts',(4.70848526800516,0.484698375887524,-5.77525567839329));
#5427=CARTESIAN_POINT('Ctrl Pts',(4.68773327755313,0.529683243661652,-5.77213956266516));
#5428=CARTESIAN_POINT('Ctrl Pts',(4.66700216788444,0.574622847378835,-5.76902658239227));
#5429=CARTESIAN_POINT('Ctrl Pts',(4.64360519704529,0.618394714065538,-5.76591360211939));
#5430=CARTESIAN_POINT('Ctrl Pts',(4.61770193321154,0.660667784337773,-5.7628006218465));
#5431=CARTESIAN_POINT('Ctrl Pts',(4.59181371917313,0.702916293957703,-5.75968945021504));
#5432=CARTESIAN_POINT('Ctrl Pts',(4.56342238277836,0.743667266039175,-5.75657827858358));
#5433=CARTESIAN_POINT('Ctrl Pts',(4.53273287956449,0.782615192544894,-5.75346710695212));
#5434=CARTESIAN_POINT('Ctrl Pts',(4.50204815845055,0.821557050106605,-5.75035642010966));
#5435=CARTESIAN_POINT('Ctrl Pts',(4.46906632132525,0.858695990482074,-5.74724573326721));
#5436=CARTESIAN_POINT('Ctrl Pts',(4.43403343612197,0.893758504170771,-5.74413504642475));
#5437=CARTESIAN_POINT('Ctrl Pts',(4.39896643785363,0.928855159775088,-5.74102133056935));
#5438=CARTESIAN_POINT('Ctrl Pts',(4.36184479304868,0.961870964602486,-5.73790761471396));
#5439=CARTESIAN_POINT('Ctrl Pts',(4.32295108406249,0.992569644240386,-5.73479389885856));
#5440=CARTESIAN_POINT('Ctrl Pts',(4.2840361546326,1.02328507310636,-5.7316784841569));
#5441=CARTESIAN_POINT('Ctrl Pts',(4.24334768554216,1.05168054557615,-5.72856306945525));
#5442=CARTESIAN_POINT('Ctrl Pts',(4.20119809161407,1.07756257194116,-5.72544765475359));
#5443=CARTESIAN_POINT('Ctrl Pts',(4.15897101688686,1.10349217551627,-5.722326513192));
#5444=CARTESIAN_POINT('Ctrl Pts',(4.11527794034272,1.12689885374361,-5.71920537163041));
#5445=CARTESIAN_POINT('Ctrl Pts',(4.07045526709899,1.14763538801389,-5.71608423006883));
#5446=CARTESIAN_POINT('Ctrl Pts',(4.0497935950466,1.1571941992045,-5.71464549385102));
#5447=CARTESIAN_POINT('Ctrl Pts',(4.02889216040453,1.16618631635696,-5.71320675763322));
#5448=CARTESIAN_POINT('Ctrl Pts',(4.00778504162465,1.17460087326884,-5.71176802141541));
#5449=CARTESIAN_POINT('Ctrl Pts',(3.99867889501626,1.17823112662949,-5.71114731410492));
#5450=CARTESIAN_POINT('Ctrl Pts',(3.98952658961544,1.18175705108102,-5.71052660679442));
#5451=CARTESIAN_POINT('Ctrl Pts',(3.98033068509731,1.1851773507521,-5.70990589948393));
#5452=CARTESIAN_POINT('',(2.27501930025681,-0.000794877133459826,-6.19341967365965));
#5453=CARTESIAN_POINT('Ctrl Pts',(3.98033068509731,1.1851773507521,-5.8467115517674));
#5454=CARTESIAN_POINT('Ctrl Pts',(4.02678408443536,1.16789959997042,-5.84982766259815));
#5455=CARTESIAN_POINT('Ctrl Pts',(4.07217160066956,1.14790474819601,-5.8529437734289));
#5456=CARTESIAN_POINT('Ctrl Pts',(4.1161668623606,1.12536107582747,-5.85605988425965));
#5457=CARTESIAN_POINT('Ctrl Pts',(4.16023964775348,1.10277767943258,-5.85918148596458));
#5458=CARTESIAN_POINT('Ctrl Pts',(4.20291481653079,1.07763678585611,-5.86230308766952));
#5459=CARTESIAN_POINT('Ctrl Pts',(4.2438935636827,1.05015084396012,-5.86542468937446));
#5460=CARTESIAN_POINT('Ctrl Pts',(4.2521753588957,1.04459594153289,-5.86605556434877));
#5461=CARTESIAN_POINT('Ctrl Pts',(4.26038797288695,1.03894538892574,-5.86668643932309));
#5462=CARTESIAN_POINT('Ctrl Pts',(4.26852910855665,1.03320113489096,-5.8673173142974));
#5463=CARTESIAN_POINT('Ctrl Pts',(4.30880622153057,1.00478225353377,-5.87043847867099));
#5464=CARTESIAN_POINT('Ctrl Pts',(4.34750735369413,0.973942382796071,-5.87355964304458));
#5465=CARTESIAN_POINT('Ctrl Pts',(4.38432675561076,0.940882666040445,-5.87668080741817));
#5466=CARTESIAN_POINT('Ctrl Pts',(4.42107892076406,0.907883320399928,-5.87979627216115));
#5467=CARTESIAN_POINT('Ctrl Pts',(4.45595576640711,0.872672532001327,-5.88291173690413));
#5468=CARTESIAN_POINT('Ctrl Pts',(4.48868260359977,0.835493147381136,-5.88602720164711));
#5469=CARTESIAN_POINT('Ctrl Pts',(4.5213765124808,0.798351171030969,-5.88913953174578));
#5470=CARTESIAN_POINT('Ctrl Pts',(4.55192433502822,0.759244929232485,-5.89225186184445));
#5471=CARTESIAN_POINT('Ctrl Pts',(4.5800880081899,0.718454239413951,-5.89536419194312));
#5472=CARTESIAN_POINT('Ctrl Pts',(4.60823533313529,0.677687227438016,-5.89847471542213));
#5473=CARTESIAN_POINT('Ctrl Pts',(4.63400093956425,0.635238154809938,-5.90158523890114));
#5474=CARTESIAN_POINT('Ctrl Pts',(4.65718850053871,0.59141799962296,-5.90469576238015));
#5475=CARTESIAN_POINT('Ctrl Pts',(4.68037247173167,0.54760462845189,-5.90780580430357));
#5476=CARTESIAN_POINT('Ctrl Pts',(4.70097893465621,0.502421080937199,-5.91091584622699));
#5477=CARTESIAN_POINT('Ctrl Pts',(4.71885746514283,0.456202974087311,-5.91402588815041));
#5478=CARTESIAN_POINT('Ctrl Pts',(4.73675346520262,0.40993970633336,-5.91713896897599));
#5479=CARTESIAN_POINT('Ctrl Pts',(4.7519160142661,0.362640373691391,-5.92025204980157));
#5480=CARTESIAN_POINT('Ctrl Pts',(4.76424351847546,0.314658906363046,-5.92336513062716));
#5481=CARTESIAN_POINT('Ctrl Pts',(4.77657776878623,0.266651181664317,-5.92647991505459));
#5482=CARTESIAN_POINT('Ctrl Pts',(4.7860737800577,0.217961117506413,-5.92959469948201));
#5483=CARTESIAN_POINT('Ctrl Pts',(4.79268115908479,0.168952595168909,-5.93270948390944));
#5484=CARTESIAN_POINT('Ctrl Pts',(4.79930071728701,0.119853736954804,-5.9358300097216));
#5485=CARTESIAN_POINT('Ctrl Pts',(4.80302097636537,0.0704357958584122,-5.93895053553375));
#5486=CARTESIAN_POINT('Ctrl Pts',(4.80384356571167,0.021065850090915,-5.94207106134591));
#5487=CARTESIAN_POINT('Ctrl Pts',(4.80422417664097,-0.00177755412125762,
-5.94351492423402));
#5488=CARTESIAN_POINT('Ctrl Pts',(4.80398515884719,-0.0246107176948163,
-5.94495878712213));
#5489=CARTESIAN_POINT('Ctrl Pts',(4.80313042611029,-0.0473976922820038,
-5.94640265001023));
#5490=CARTESIAN_POINT('Ctrl Pts',(4.80128205614194,-0.0966748027493485,
-5.94952502111592));
#5491=CARTESIAN_POINT('Ctrl Pts',(4.79654284474449,-0.145951235456336,-5.9526473922216));
#5492=CARTESIAN_POINT('Ctrl Pts',(4.7889147137975,-0.194860787078774,-5.95576976332729));
#5493=CARTESIAN_POINT('Ctrl Pts',(4.78130052307174,-0.243680957701523,-5.95888642837676));
#5494=CARTESIAN_POINT('Ctrl Pts',(4.77080796784645,-0.292135040197593,-5.96200309342623));
#5495=CARTESIAN_POINT('Ctrl Pts',(4.75749086411774,-0.339860134533483,-5.9651197584757));
#5496=CARTESIAN_POINT('Ctrl Pts',(4.74418717573548,-0.387537151698246,-5.96823328386791));
#5497=CARTESIAN_POINT('Ctrl Pts',(4.72806471860148,-0.434486109513725,-5.97134680926013));
#5498=CARTESIAN_POINT('Ctrl Pts',(4.70922827104811,-0.480354649383736,-5.97446033465234));
#5499=CARTESIAN_POINT('Ctrl Pts',(4.69040279690021,-0.526196467968576,-5.97757204622183));
#5500=CARTESIAN_POINT('Ctrl Pts',(4.66886667241962,-0.570958609873898,-5.98068375779132));
#5501=CARTESIAN_POINT('Ctrl Pts',(4.64477355657755,-0.614306704037186,-5.98379546936081));
#5502=CARTESIAN_POINT('Ctrl Pts',(4.62068424206337,-0.657647958889199,-5.98690668997528));
#5503=CARTESIAN_POINT('Ctrl Pts',(4.59403900408932,-0.699575131033123,-5.99001791058976));
#5504=CARTESIAN_POINT('Ctrl Pts',(4.56503719138121,-0.739778880859403,-5.99312913120424));
#5505=CARTESIAN_POINT('Ctrl Pts',(4.53600726781207,-0.780021599354146,-5.99624336746092));
#5506=CARTESIAN_POINT('Ctrl Pts',(4.50461653120828,-0.818537116168381,-5.9993576037176));
#5507=CARTESIAN_POINT('Ctrl Pts',(4.47110631650094,-0.855047025421062,-6.00247183997428));
#5508=CARTESIAN_POINT('Ctrl Pts',(4.43757789602443,-0.891576770147373,-6.00558776816481));
#5509=CARTESIAN_POINT('Ctrl Pts',(4.40192809828093,-0.926098356163972,-6.00870369635533));
#5510=CARTESIAN_POINT('Ctrl Pts',(4.36443453707344,-0.958370851958811,-6.01181962454586));
#5511=CARTESIAN_POINT('Ctrl Pts',(4.32687226299319,-0.990702492199404,-6.01494126316693));
#5512=CARTESIAN_POINT('Ctrl Pts',(4.28745991766333,-1.02077648414758,-6.018062901788));
#5513=CARTESIAN_POINT('Ctrl Pts',(4.24650618298384,-1.04839374492286,-6.02118454040908));
#5514=CARTESIAN_POINT('Ctrl Pts',(4.22768677657697,-1.06108466208688,-6.0226190221804));
#5515=CARTESIAN_POINT('Ctrl Pts',(4.20854224778094,-1.0732574273192,-6.02405350395173));
#5516=CARTESIAN_POINT('Ctrl Pts',(4.18910421403698,-1.08489601585248,-6.02548798572305));
#5517=CARTESIAN_POINT('Ctrl Pts',(4.14679330469148,-1.11022981611375,-6.02861043262194));
#5518=CARTESIAN_POINT('Ctrl Pts',(4.1029060216482,-1.13313989086988,-6.03173287952083));
#5519=CARTESIAN_POINT('Ctrl Pts',(4.05775042182792,-1.15342814934081,-6.03485532641971));
#5520=CARTESIAN_POINT('Ctrl Pts',(4.01267703349248,-1.1736794704693,-6.03797208850881));
#5521=CARTESIAN_POINT('Ctrl Pts',(3.96634040393713,-1.19131822019731,-6.04108885059791));
#5522=CARTESIAN_POINT('Ctrl Pts',(3.9190741173137,-1.20619161048218,-6.04420561268701));
#5523=CARTESIAN_POINT('Ctrl Pts',(3.87185524659392,-1.22105008029642,-6.0473192481482));
#5524=CARTESIAN_POINT('Ctrl Pts',(3.82370908510954,-1.23314851921892,-6.05043288360939));
#5525=CARTESIAN_POINT('Ctrl Pts',(3.77498816693699,-1.24238260820414,-6.05354651907058));
#5526=CARTESIAN_POINT('Ctrl Pts',(3.72629543266342,-1.25161135548725,-6.05665835336728));
#5527=CARTESIAN_POINT('Ctrl Pts',(3.67702913750895,-1.25797893382598,-6.05977018766399));
#5528=CARTESIAN_POINT('Ctrl Pts',(3.62755338927646,-1.2614318075832,-6.0628820219607));
#5529=CARTESIAN_POINT('Ctrl Pts',(3.57808525121624,-1.26488415023246,-6.06599337760684));
#5530=CARTESIAN_POINT('Ctrl Pts',(3.52840827013993,-1.26542264149081,-6.06910473325298));
#5531=CARTESIAN_POINT('Ctrl Pts',(3.47889048383974,-1.26304569470548,-6.07221608889912));
#5532=CARTESIAN_POINT('Ctrl Pts',(3.42932442986109,-1.26066643098089,-6.07533047735276));
#5533=CARTESIAN_POINT('Ctrl Pts',(3.37991842841813,-1.25536608318217,-6.0784448658064));
#5534=CARTESIAN_POINT('Ctrl Pts',(3.33103748293375,-1.24719512748296,-6.08155925426005));
#5535=CARTESIAN_POINT('Ctrl Pts',(3.28212982503215,-1.23901970652687,-6.08467534466202));
#5536=CARTESIAN_POINT('Ctrl Pts',(3.2337483288176,-1.22797067597364,-6.087791435064));
#5537=CARTESIAN_POINT('Ctrl Pts',(3.18624636692195,-1.21414935699525,-6.09090752546598));
#5538=CARTESIAN_POINT('Ctrl Pts',(3.13865715259362,-1.20030265077693,-6.0940293395572));
#5539=CARTESIAN_POINT('Ctrl Pts',(3.09195121267526,-1.18367367764803,-6.09715115364841));
#5540=CARTESIAN_POINT('Ctrl Pts',(3.04646378297013,-1.16441262155517,-6.10027296773963));
#5541=CARTESIAN_POINT('Ctrl Pts',(3.02557720540658,-1.15556847395995,-6.10170641897171));
#5542=CARTESIAN_POINT('Ctrl Pts',(3.00494721266106,-1.14617002862237,-6.1031398702038));
#5543=CARTESIAN_POINT('Ctrl Pts',(2.98460441055827,-1.13623500758593,-6.10457332143588));
#5544=CARTESIAN_POINT('Ctrl Pts',(2.94035875657203,-1.1146263078157,-6.10769108205217));
#5545=CARTESIAN_POINT('Ctrl Pts',(2.89727891392357,-1.09038131290469,-6.11080884266845));
#5546=CARTESIAN_POINT('Ctrl Pts',(2.85569836475949,-1.06364915261504,-6.11392660328474));
#5547=CARTESIAN_POINT('Ctrl Pts',(2.8141938897277,-1.03696590043122,-6.1170386597692));
#5548=CARTESIAN_POINT('Ctrl Pts',(2.77418372665897,-1.00780480194085,-6.12015071625367));
#5549=CARTESIAN_POINT('Ctrl Pts',(2.73597740755509,-0.976361141267487,-6.12326277273813));
#5550=CARTESIAN_POINT('Ctrl Pts',(2.69780957157364,-0.944949152062927,-6.12637169461938));
#5551=CARTESIAN_POINT('Ctrl Pts',(2.66144240521671,-0.911259499285034,-6.12948061650063));
#5552=CARTESIAN_POINT('Ctrl Pts',(2.6271552208983,-0.875529835342595,-6.13258953838188));
#5553=CARTESIAN_POINT('Ctrl Pts',(2.59288789143865,-0.839820861563135,-6.13569665996351));
#5554=CARTESIAN_POINT('Ctrl Pts',(2.56069853780505,-0.802074612489938,-6.13880378154514));
#5555=CARTESIAN_POINT('Ctrl Pts',(2.53083026355083,-0.76256618154647,-6.14191090312677));
#5556=CARTESIAN_POINT('Ctrl Pts',(2.50096649733004,-0.723063713630052,-6.145017555749));
#5557=CARTESIAN_POINT('Ctrl Pts',(2.47342344525313,-0.681800030670023,-6.14812420837123));
#5558=CARTESIAN_POINT('Ctrl Pts',(2.44840283402651,-0.639081882325442,-6.15123086099346));
#5559=CARTESIAN_POINT('Ctrl Pts',(2.42335738307379,-0.596321324661008,-6.15434059780894));
#5560=CARTESIAN_POINT('Ctrl Pts',(2.40083964946336,-0.552103894614342,-6.15745033462442));
#5561=CARTESIAN_POINT('Ctrl Pts',(2.38100607732538,-0.506762213631349,-6.1605600714399));
#5562=CARTESIAN_POINT('Ctrl Pts',(2.36116150573799,-0.461395386722895,-6.16367153287627));
#5563=CARTESIAN_POINT('Ctrl Pts',(2.34400424945267,-0.41490358359502,-6.16678299431264));
#5564=CARTESIAN_POINT('Ctrl Pts',(2.32964178545537,-0.367637394336423,-6.16989445574901));
#5565=CARTESIAN_POINT('Ctrl Pts',(2.31525249379191,-0.32028291649819,-6.17301172908845));
#5566=CARTESIAN_POINT('Ctrl Pts',(2.30366854040601,-0.272151700368794,-6.1761290024279));
#5567=CARTESIAN_POINT('Ctrl Pts',(2.29494654851669,-0.223605763563201,-6.17924627576734));
#5568=CARTESIAN_POINT('Ctrl Pts',(2.29083133302437,-0.200700790276553,-6.18071706956113));
#5569=CARTESIAN_POINT('Ctrl Pts',(2.28735248171025,-0.177703579422882,-6.18218786335492));
#5570=CARTESIAN_POINT('Ctrl Pts',(2.28451191880524,-0.154652350737349,-6.1836586571487));
#5571=CARTESIAN_POINT('Ctrl Pts',(2.27822806006649,-0.103658702767496,-6.18691232930561));
#5572=CARTESIAN_POINT('Ctrl Pts',(2.27505166281584,-0.0522775696465564,
-6.19016600146251));
#5573=CARTESIAN_POINT('Ctrl Pts',(2.27501930025721,-0.000794877769987878,
-6.19341967361942));
#5574=CARTESIAN_POINT('Ctrl Pts',(2.27501930025681,-0.000794877133460714,
-6.19341967365965));
#5575=CARTESIAN_POINT('Ctrl Pts',(2.27498866481498,0.0479403385423533,-6.19649970713347));
#5576=CARTESIAN_POINT('Ctrl Pts',(2.27777974167085,0.0967837354840311,-6.19957974060728));
#5577=CARTESIAN_POINT('Ctrl Pts',(2.28340368707692,0.145376903137893,-6.2026597740811));
#5578=CARTESIAN_POINT('Ctrl Pts',(2.28902068514398,0.193910042967064,-6.20573600274617));
#5579=CARTESIAN_POINT('Ctrl Pts',(2.29746356813488,0.242193009571163,-6.20881223141124));
#5580=CARTESIAN_POINT('Ctrl Pts',(2.30869149746577,0.28986856483816,-6.21188846007631));
#5581=CARTESIAN_POINT('Ctrl Pts',(2.31991062224023,0.337506734572732,-6.21496227646855));
#5582=CARTESIAN_POINT('Ctrl Pts',(2.33391034355925,0.384537889114209,-6.21803609286079));
#5583=CARTESIAN_POINT('Ctrl Pts',(2.35059855415923,0.430613868290296,-6.22110990925304));
#5584=CARTESIAN_POINT('Ctrl Pts',(2.36728120520785,0.476674497601834,-6.22418270162656));
#5585=CARTESIAN_POINT('Ctrl Pts',(2.38665037854992,0.521780053466338,-6.22725549400008));
#5586=CARTESIAN_POINT('Ctrl Pts',(2.4085646527477,0.565599151678052,-6.2303282863736));
#5587=CARTESIAN_POINT('Ctrl Pts',(2.43049637673816,0.60945314195016,-6.23340352553543));
#5588=CARTESIAN_POINT('Ctrl Pts',(2.45497699765719,0.652018123811447,-6.23647876469726));
#5589=CARTESIAN_POINT('Ctrl Pts',(2.48181851722148,0.692986170183253,-6.23955400385908));
#5590=CARTESIAN_POINT('Ctrl Pts',(2.50867171307318,0.733972038000772,-6.24263058077588));
#5591=CARTESIAN_POINT('Ctrl Pts',(2.53788751699157,0.773359134237717,-6.24570715769268));
#5592=CARTESIAN_POINT('Ctrl Pts',(2.56923596999665,0.810870516074163,-6.24878373460948));
#5593=CARTESIAN_POINT('Ctrl Pts',(2.60064014758636,0.84844857763388,-6.25186578040766));
#5594=CARTESIAN_POINT('Ctrl Pts',(2.63418415230918,0.884143862022931,-6.25494782620583));
#5595=CARTESIAN_POINT('Ctrl Pts',(2.66960061631979,0.91771573376914,-6.25802987200401));
#5596=CARTESIAN_POINT('Ctrl Pts',(2.68765761510404,0.934832271634837,-6.25960124562318));
#5597=CARTESIAN_POINT('Ctrl Pts',(2.70620080772796,0.951397482579278,-6.26117261924236));
#5598=CARTESIAN_POINT('Ctrl Pts',(2.72519170678115,0.967383702259465,-6.26274399286153));
#5599=CARTESIAN_POINT('Ctrl Pts',(2.76296112936729,0.999177367475883,-6.26586916740419));
#5600=CARTESIAN_POINT('Ctrl Pts',(2.80267577049992,1.02882352473978,-6.26899434194685));
#5601=CARTESIAN_POINT('Ctrl Pts',(2.84406211499685,1.05607760177351,-6.27211951648951));
#5602=CARTESIAN_POINT('Ctrl Pts',(2.88537441929957,1.08328292124767,-6.27523910009311));
#5603=CARTESIAN_POINT('Ctrl Pts',(2.92835204198969,1.10810435070506,-6.27835868369671));
#5604=CARTESIAN_POINT('Ctrl Pts',(2.97268912824492,1.13033804205804,-6.28147826730031));
#5605=CARTESIAN_POINT('Ctrl Pts',(3.01698256327074,1.15254984365588,-6.2845947795776));
#5606=CARTESIAN_POINT('Ctrl Pts',(3.0626323255472,1.17217870774427,-6.28771129185488));
#5607=CARTESIAN_POINT('Ctrl Pts',(3.10930621329362,1.18906566882115,-6.29082780413217));
#5608=CARTESIAN_POINT('Ctrl Pts',(3.15595385882097,1.20594313526725,-6.29394256416207));
#5609=CARTESIAN_POINT('Ctrl Pts',(3.20362397598171,1.22008156773149,-6.29705732419197));
#5610=CARTESIAN_POINT('Ctrl Pts',(3.25196492088847,1.23137032309035,-6.30017208422187));
#5611=CARTESIAN_POINT('Ctrl Pts',(3.30029909838449,1.24265749809857,-6.30328640820609));
#5612=CARTESIAN_POINT('Ctrl Pts',(3.34930338505032,1.25109566524075,-6.3064007321903));
#5613=CARTESIAN_POINT('Ctrl Pts',(3.39861404298749,1.25662485606469,-6.30951505617452));
#5614=CARTESIAN_POINT('Ctrl Pts',(3.44797333837544,1.26215950059292,-6.31263245196483));
#5615=CARTESIAN_POINT('Ctrl Pts',(3.49763906418198,1.26477938096814,-6.31574984775513));
#5616=CARTESIAN_POINT('Ctrl Pts',(3.54724222921144,1.2644764143745,-6.31886724354544));
#5617=CARTESIAN_POINT('Ctrl Pts',(3.59687289428225,1.2641732798159,-6.32198636762291));
#5618=CARTESIAN_POINT('Ctrl Pts',(3.64644038379152,1.26094410710264,-6.32510549170037));
#5619=CARTESIAN_POINT('Ctrl Pts',(3.69557912019877,1.25483285923727,-6.32822461577784));
#5620=CARTESIAN_POINT('Ctrl Pts',(3.7448080925388,1.24871038898012,-6.3313494676597));
#5621=CARTESIAN_POINT('Ctrl Pts',(3.793606203084,1.23969538077051,-6.33447431954156));
#5622=CARTESIAN_POINT('Ctrl Pts',(3.84161801442852,1.22788292029281,-6.33759917142343));
#5623=CARTESIAN_POINT('Ctrl Pts',(3.86328277537995,1.22255268747444,-6.33900922380707));
#5624=CARTESIAN_POINT('Ctrl Pts',(3.88478764633446,1.21665352349932,-6.34041927619071));
#5625=CARTESIAN_POINT('Ctrl Pts',(3.90610121351515,1.21019740856716,-6.34182932857435));
#5626=CARTESIAN_POINT('Ctrl Pts',(3.93106378827338,1.20263596893224,-6.34348079018757));
#5627=CARTESIAN_POINT('Ctrl Pts',(3.95582479527397,1.19429200464362,-6.34513225180078));
#5628=CARTESIAN_POINT('Ctrl Pts',(3.98033068509731,1.1851773507521,-6.346783713414));
#5629=CARTESIAN_POINT('Origin',(3.53951905042299,8.32667268468867E-16,-7.60421172358873));
#5630=CARTESIAN_POINT('',(1.99651962906757,0.00133629967821312,-5.85421172358873));
#5631=CARTESIAN_POINT('Ctrl Pts',(4.4805026613161,-1.22496740309806,-6.17703688246106));
#5632=CARTESIAN_POINT('Ctrl Pts',(4.8351830152191,-0.947966885397602,-6.15375615496722));
#5633=CARTESIAN_POINT('Ctrl Pts',(5.3296905430907,-0.00766043899371661,
-6.10411364890244));
#5634=CARTESIAN_POINT('Ctrl Pts',(4.58962568481027,1.48829617865197,-6.02810936426672));
#5635=CARTESIAN_POINT('Ctrl Pts',(2.86500634349213,1.69194423152176,-5.94902402855389));
#5636=CARTESIAN_POINT('Ctrl Pts',(2.05033956475987,0.713964383672213,-5.8910581483279));
#5637=CARTESIAN_POINT('Ctrl Pts',(1.99506637965176,0.10286799783797,-5.85945404667284));
#5638=CARTESIAN_POINT('Ctrl Pts',(1.99598824456801,0.00133675987860297,
-5.85421172358873));
#5639=CARTESIAN_POINT('Ctrl Pts',(1.99651962906757,0.00133629967821312,
-5.85421172358873));
#5640=CARTESIAN_POINT('Ctrl Pts',(1.99647063856088,-0.0552320919015559,
-5.85128991870194));
#5641=CARTESIAN_POINT('Ctrl Pts',(1.99953669991828,-0.111900437912663,-5.84836811381516));
#5642=CARTESIAN_POINT('Ctrl Pts',(2.00572420093829,-0.168292482583732,-5.84544630892837));
#5643=CARTESIAN_POINT('Ctrl Pts',(2.01190613034431,-0.22463374832097,-5.84252713501796));
#5644=CARTESIAN_POINT('Ctrl Pts',(2.02120387741375,-0.280698672975614,-5.83960796110754));
#5645=CARTESIAN_POINT('Ctrl Pts',(2.03357181527654,-0.336112964574063,-5.83668878719712));
#5646=CARTESIAN_POINT('Ctrl Pts',(2.04593370493793,-0.39150015733038,-5.83377104082879));
#5647=CARTESIAN_POINT('Ctrl Pts',(2.06136269399849,-0.446236823221072,-5.83085329446045));
#5648=CARTESIAN_POINT('Ctrl Pts',(2.07976194100033,-0.499958179741059,-5.82793554809211));
#5649=CARTESIAN_POINT('Ctrl Pts',(2.09815975929864,-0.55367536479188,-5.82501802828709));
#5650=CARTESIAN_POINT('Ctrl Pts',(2.11952720091026,-0.606376889209763,-5.82210050848208));
#5651=CARTESIAN_POINT('Ctrl Pts',(2.14371812919713,-0.657714822932431,-5.81918298867706));
#5652=CARTESIAN_POINT('Ctrl Pts',(2.1679326246043,-0.709102770744913,-5.81626262658591));
#5653=CARTESIAN_POINT('Ctrl Pts',(2.19497586222247,-0.759123991599414,-5.81334226449475));
#5654=CARTESIAN_POINT('Ctrl Pts',(2.22465502102199,-0.807453765975103,-5.81042190240359));
#5655=CARTESIAN_POINT('Ctrl Pts',(2.25435184685727,-0.855812309490017,-5.80749980191608));
#5656=CARTESIAN_POINT('Ctrl Pts',(2.28668740535122,-0.902476964311451,-5.80457770142857));
#5657=CARTESIAN_POINT('Ctrl Pts',(2.3214265789633,-0.947153488603201,-5.80165560094106));
#5658=CARTESIAN_POINT('Ctrl Pts',(2.35622433730217,-0.991905356137118,-5.79872857257412));
#5659=CARTESIAN_POINT('Ctrl Pts',(2.39343343625151,-1.03466200763537,-5.79580154420719));
#5660=CARTESIAN_POINT('Ctrl Pts',(2.43278086258591,-1.07516490994781,-5.79287451584026));
#5661=CARTESIAN_POINT('Ctrl Pts',(2.44183753298804,-1.08448753840783,-5.79220079626958));
#5662=CARTESIAN_POINT('Ctrl Pts',(2.45100735116571,-1.09369093355053,-5.79152707669891));
#5663=CARTESIAN_POINT('Ctrl Pts',(2.46028674854408,-1.10277225145592,-5.79085335712824));
#5664=CARTESIAN_POINT('Ctrl Pts',(2.50119736372677,-1.14280958222535,-5.78788309074425));
#5665=CARTESIAN_POINT('Ctrl Pts',(2.54442403981831,-1.18065055045223,-5.78491282436025));
#5666=CARTESIAN_POINT('Ctrl Pts',(2.5897016260704,-1.21601638985509,-5.78194255797625));
#5667=CARTESIAN_POINT('Ctrl Pts',(2.63489924292426,-1.25131976601445,-5.77897753768497));
#5668=CARTESIAN_POINT('Ctrl Pts',(2.68214017261957,-1.28415637209005,-5.77601251739368));
#5669=CARTESIAN_POINT('Ctrl Pts',(2.73112360642299,-1.3142852833841,-5.7730474971024));
#5670=CARTESIAN_POINT('Ctrl Pts',(2.78005870122236,-1.3443844621451,-5.77008540282337));
#5671=CARTESIAN_POINT('Ctrl Pts',(2.83073245125779,-1.37178096864678,-5.76712330854435));
#5672=CARTESIAN_POINT('Ctrl Pts',(2.88281369051602,-1.39627614398781,-5.76416121426532));
#5673=CARTESIAN_POINT('Ctrl Pts',(2.93486358072305,-1.42075657504631,-5.76120090294781));
#5674=CARTESIAN_POINT('Ctrl Pts',(2.98831880993198,-1.4423389154832,-5.7582405916303));
#5675=CARTESIAN_POINT('Ctrl Pts',(3.04282409600851,-1.46087067266723,-5.75528028031279));
#5676=CARTESIAN_POINT('Ctrl Pts',(3.09731755283789,-1.47939840791592,-5.75232061146974));
#5677=CARTESIAN_POINT('Ctrl Pts',(3.15286012075714,-1.49487670675489,-5.74936094262669));
#5678=CARTESIAN_POINT('Ctrl Pts',(3.20907914364962,-1.50720219878144,-5.74640127378364));
#5679=CARTESIAN_POINT('Ctrl Pts',(3.26534886690617,-1.51953880638597,-5.74343893580334));
#5680=CARTESIAN_POINT('Ctrl Pts',(3.32229575398386,-1.52871681276762,-5.74047659782305));
#5681=CARTESIAN_POINT('Ctrl Pts',(3.37953602790866,-1.53468382167376,-5.73751425984275));
#5682=CARTESIAN_POINT('Ctrl Pts',(3.43680046940972,-1.54065334992743,-5.73455067112545));
#5683=CARTESIAN_POINT('Ctrl Pts',(3.49435802300424,-1.54340915196995,-5.73158708240814));
#5684=CARTESIAN_POINT('Ctrl Pts',(3.55182208858797,-1.54295095037137,-5.72862349369083));
#5685=CARTESIAN_POINT('Ctrl Pts',(3.60939633838999,-1.54249187019616,-5.72565422245346));
#5686=CARTESIAN_POINT('Ctrl Pts',(3.6668762199932,-1.53880650470921,-5.72268495121608));
#5687=CARTESIAN_POINT('Ctrl Pts',(3.72387841604006,-1.53194667802416,-5.7197156799787));
#5688=CARTESIAN_POINT('Ctrl Pts',(3.77473646114266,-1.52582625812565,-5.71706646045761));
#5689=CARTESIAN_POINT('Ctrl Pts',(3.82521408602547,-1.51717961894724,-5.71441724093651));
#5690=CARTESIAN_POINT('Ctrl Pts',(3.87504773869695,-1.50607752102777,-5.71176802141542));
#5691=CARTESIAN_POINT('Ctrl Pts',(3.93090212592116,-1.49363410492333,-5.70879873208902));
#5692=CARTESIAN_POINT('Ctrl Pts',(3.98617942899864,-1.47805350283576,-5.70582944276262));
#5693=CARTESIAN_POINT('Ctrl Pts',(4.04050175195703,-1.45940581496842,-5.70286015343622));
#5694=CARTESIAN_POINT('Ctrl Pts',(4.09474970761238,-1.44078365580052,-5.69989492906925));
#5695=CARTESIAN_POINT('Ctrl Pts',(4.14804478403148,-1.41910289486014,-5.69692970470228));
#5696=CARTESIAN_POINT('Ctrl Pts',(4.20002090048548,-1.39448424374893,-5.69396448033531));
#5697=CARTESIAN_POINT('Ctrl Pts',(4.2519448213428,-1.36989031524633,-5.691002233714));
#5698=CARTESIAN_POINT('Ctrl Pts',(4.30255193818079,-1.34236456518616,-5.68803998709269));
#5699=CARTESIAN_POINT('Ctrl Pts',(4.35149505667516,-1.31207620406391,-5.68507774047138));
#5700=CARTESIAN_POINT('Ctrl Pts',(4.39558502363139,-1.28479120706905,-5.68240922731432));
#5701=CARTESIAN_POINT('Ctrl Pts',(4.43832462406854,-1.25526506293894,-5.67974071415726));
#5702=CARTESIAN_POINT('Ctrl Pts',(4.47947725029973,-1.22365337513712,-5.6770722010002));
#5703=CARTESIAN_POINT('',(1.99651939415668,-0.0010299330301491,-5.89578827637539));
#5704=CARTESIAN_POINT('Ctrl Pts',(1.99651939415668,-0.00102993303015119,
-5.89578827637539));
#5705=CARTESIAN_POINT('Ctrl Pts',(1.99656311124628,-0.0665249237226865,
-5.89242280315063));
#5706=CARTESIAN_POINT('Ctrl Pts',(2.00078094053252,-0.131858231058162,-5.88905732992587));
#5707=CARTESIAN_POINT('Ctrl Pts',(2.00908724191393,-0.196538748097368,-5.88569185670111));
#5708=CARTESIAN_POINT('Ctrl Pts',(2.01746504072735,-0.261776010029041,-5.88229741478355));
#5709=CARTESIAN_POINT('Ctrl Pts',(2.03000187710493,-0.326348970253648,-5.87890297286599));
#5710=CARTESIAN_POINT('Ctrl Pts',(2.04656016328037,-0.389772704665002,-5.87550853094842));
#5711=CARTESIAN_POINT('Ctrl Pts',(2.0598792412247,-0.440789195936822,-5.87277812539808));
#5712=CARTESIAN_POINT('Ctrl Pts',(2.07579929237439,-0.491062442571037,-5.87004771984774));
#5713=CARTESIAN_POINT('Ctrl Pts',(2.09422649337875,-0.54035027949703,-5.8673173142974));
#5714=CARTESIAN_POINT('Ctrl Pts',(2.11427285398687,-0.593968935546792,-5.86434699372318));
#5715=CARTESIAN_POINT('Ctrl Pts',(2.13734871336475,-0.646582004481705,-5.86137667314896));
#5716=CARTESIAN_POINT('Ctrl Pts',(2.16333231133361,-0.697824518883177,-5.85840635257474));
#5717=CARTESIAN_POINT('Ctrl Pts',(2.18927003388335,-0.74897656191007,-5.8554412762589));
#5718=CARTESIAN_POINT('Ctrl Pts',(2.21810507132652,-0.798762392239985,-5.85247619994305));
#5719=CARTESIAN_POINT('Ctrl Pts',(2.24966731486717,-0.846836170864018,-5.84951112362721));
#5720=CARTESIAN_POINT('Ctrl Pts',(2.28119842340232,-0.894862526453641,-5.84654897225133));
#5721=CARTESIAN_POINT('Ctrl Pts',(2.31545112299997,-0.941179742998912,-5.84358682087544));
#5722=CARTESIAN_POINT('Ctrl Pts',(2.35220987785363,-0.985467365635541,-5.84062466949955));
#5723=CARTESIAN_POINT('Ctrl Pts',(2.38894651900094,-1.02972834527281,-5.83766430012488));
#5724=CARTESIAN_POINT('Ctrl Pts',(2.42818589452722,-1.07196175113325,-5.83470393075021));
#5725=CARTESIAN_POINT('Ctrl Pts',(2.46967103689842,-1.11187869300456,-5.83174356137554));
#5726=CARTESIAN_POINT('Ctrl Pts',(2.51114718785878,-1.15178698335383,-5.82878383362569));
#5727=CARTESIAN_POINT('Ctrl Pts',(2.55486776378531,-1.18937944535614,-5.82582410587584));
#5728=CARTESIAN_POINT('Ctrl Pts',(2.60053921513923,-1.2244042914538,-5.82286437812599));
#5729=CARTESIAN_POINT('Ctrl Pts',(2.64625186667548,-1.25946073343909,-5.81990198040794));
#5730=CARTESIAN_POINT('Ctrl Pts',(2.69391849626159,-1.29194461244608,-5.81693958268989));
#5731=CARTESIAN_POINT('Ctrl Pts',(2.74321384782584,-1.32164557439455,-5.81397718497184));
#5732=CARTESIAN_POINT('Ctrl Pts',(2.79253002127664,-1.35135908174621,-5.81101353596523));
#5733=CARTESIAN_POINT('Ctrl Pts',(2.84347582688872,-1.3782870836566,-5.80804988695863));
#5734=CARTESIAN_POINT('Ctrl Pts',(2.89570132904561,-1.40226521800993,-5.80508623795202));
#5735=CARTESIAN_POINT('Ctrl Pts',(2.94802697090794,-1.42628932919856,-5.80211690630138));
#5736=CARTESIAN_POINT('Ctrl Pts',(3.00163672595878,-1.44735207851464,-5.79914757465073));
#5737=CARTESIAN_POINT('Ctrl Pts',(3.0561615146613,-1.46533767187716,-5.79617824300008));
#5738=CARTESIAN_POINT('Ctrl Pts',(3.10479966393815,-1.48138149333188,-5.79352948819492));
#5739=CARTESIAN_POINT('Ctrl Pts',(3.15416545298975,-1.49497737112332,-5.79088073338975));
#5740=CARTESIAN_POINT('Ctrl Pts',(3.20399036525539,-1.50607752171981,-5.78823197858458));
#5741=CARTESIAN_POINT('Ctrl Pts',(3.25984361339259,-1.51852068393395,-5.78526274988631));
#5742=CARTESIAN_POINT('Ctrl Pts',(3.31650607033671,-1.5278785066749,-5.78229352118805));
#5743=CARTESIAN_POINT('Ctrl Pts',(3.37360583569431,-1.53405404245691,-5.77932429248978));
#5744=CARTESIAN_POINT('Ctrl Pts',(3.43062525672136,-1.54022088872356,-5.77635924175426));
#5745=CARTESIAN_POINT('Ctrl Pts',(3.48808025361493,-1.54321426355827,-5.77339419101873));
#5746=CARTESIAN_POINT('Ctrl Pts',(3.545588182638,-1.54298806399601,-5.7704291402832));
#5747=CARTESIAN_POINT('Ctrl Pts',(3.60303733296054,-1.54276209563171,-5.76746712011811));
#5748=CARTESIAN_POINT('Ctrl Pts',(3.66053878950446,-1.53932307715738,-5.76450509995301));
#5749=CARTESIAN_POINT('Ctrl Pts',(3.71770644176347,-1.53267682619895,-5.76154307978792));
#5750=CARTESIAN_POINT('Ctrl Pts',(3.77483766885917,-1.52603480999158,-5.7585829469151));
#5751=CARTESIAN_POINT('Ctrl Pts',(3.83163499688114,-1.51618967455776,-5.75562281404227));
#5752=CARTESIAN_POINT('Ctrl Pts',(3.88771620729142,-1.50319916842338,-5.75266268116945));
#5753=CARTESIAN_POINT('Ctrl Pts',(3.94381019864848,-1.49020570174363,-5.74970187368028));
#5754=CARTESIAN_POINT('Ctrl Pts',(3.99918723471621,-1.47406553478078,-5.74674106619112));
#5755=CARTESIAN_POINT('Ctrl Pts',(4.05347574099386,-1.4548874596399,-5.74378025870196));
#5756=CARTESIAN_POINT('Ctrl Pts',(4.10776768221337,-1.43570817106403,-5.74081926387662));
#5757=CARTESIAN_POINT('Ctrl Pts',(4.16097046861186,-1.41349077698758,-5.73785826905127));
#5758=CARTESIAN_POINT('Ctrl Pts',(4.21273086404559,-1.38839290332347,-5.73489727422593));
#5759=CARTESIAN_POINT('Ctrl Pts',(4.26455729142666,-1.36326301171478,-5.73193250199022));
#5760=CARTESIAN_POINT('Ctrl Pts',(4.31493718855317,-1.33524554149718,-5.7289677297545));
#5761=CARTESIAN_POINT('Ctrl Pts',(4.36354152761078,-1.30454434845631,-5.72600295751879));
#5762=CARTESIAN_POINT('Ctrl Pts',(4.40343807886671,-1.27934347656869,-5.72356934377653));
#5763=CARTESIAN_POINT('Ctrl Pts',(4.44213866194226,-1.252335282131,-5.72113573003426));
#5764=CARTESIAN_POINT('Ctrl Pts',(4.47947725029973,-1.22365337513712,-5.718702116292));
#5765=CARTESIAN_POINT('Ctrl Pts',(4.47947725029973,-1.22365337513712,-6.21868039134515));
#5766=CARTESIAN_POINT('Ctrl Pts',(4.52523315907666,-1.1885056425181,-6.21571279242732));
#5767=CARTESIAN_POINT('Ctrl Pts',(4.56900329419267,-1.15079704745477,-6.21274519350949));
#5768=CARTESIAN_POINT('Ctrl Pts',(4.61049943673485,-1.11078801404016,-6.20977759459167));
#5769=CARTESIAN_POINT('Ctrl Pts',(4.65201300551891,-1.0707621788929,-6.20680874943519));
#5770=CARTESIAN_POINT('Ctrl Pts',(4.6912503230112,-1.02843436000381,-6.20383990427871));
#5771=CARTESIAN_POINT('Ctrl Pts',(4.72796119069533,-0.984100746481225,-6.20087105912224));
#5772=CARTESIAN_POINT('Ctrl Pts',(4.76474313047905,-0.939681303252234,-6.19789646629288));
#5773=CARTESIAN_POINT('Ctrl Pts',(4.79898853545788,-0.89324872378389,-6.19492187346353));
#5774=CARTESIAN_POINT('Ctrl Pts',(4.83048911952562,-0.845130333546938,-6.19194728063417));
#5775=CARTESIAN_POINT('Ctrl Pts',(4.85974763162996,-0.800436797066403,-6.18918440613901));
#5776=CARTESIAN_POINT('Ctrl Pts',(4.88663845078139,-0.754289480962414,-6.18642153164386));
#5777=CARTESIAN_POINT('Ctrl Pts',(4.91103098090795,-0.706968192026646,-6.18365865714871));
#5778=CARTESIAN_POINT('Ctrl Pts',(4.93722198129047,-0.656157886978836,-6.18069207489651));
#5779=CARTESIAN_POINT('Ctrl Pts',(4.96064138038873,-0.603781949096697,-6.17772549264432));
#5780=CARTESIAN_POINT('Ctrl Pts',(4.98110043515803,-0.550174618812436,-6.17475891039213));
#5781=CARTESIAN_POINT('Ctrl Pts',(5.00152279065203,-0.496663448893067,-6.1717976495695));
#5782=CARTESIAN_POINT('Ctrl Pts',(5.01899515628914,-0.441925754840174,-6.16883638874687));
#5783=CARTESIAN_POINT('Ctrl Pts',(5.03337538817453,-0.386318834849605,-6.16587512792423));
#5784=CARTESIAN_POINT('Ctrl Pts',(5.04774120080218,-0.330767672688111,-6.16291683639885));
#5785=CARTESIAN_POINT('Ctrl Pts',(5.05902089194744,-0.27434951481704,-6.15995854487347));
#5786=CARTESIAN_POINT('Ctrl Pts',(5.06712160528695,-0.217438346142331,-6.15700025334809));
#5787=CARTESIAN_POINT('Ctrl Pts',(5.07521733588585,-0.160562183470108,-6.15404378146485));
#5788=CARTESIAN_POINT('Ctrl Pts',(5.08013789098226,-0.103194127555836,-6.15108730958161));
#5789=CARTESIAN_POINT('Ctrl Pts',(5.08184161392253,-0.045717722167791,-6.14813083769836));
#5790=CARTESIAN_POINT('Ctrl Pts',(5.08354494926005,0.0117456071428263,-6.14517503842251));
#5791=CARTESIAN_POINT('Ctrl Pts',(5.08203288981773,0.0693167147109322,-6.14221923914666));
#5792=CARTESIAN_POINT('Ctrl Pts',(5.07731583509648,0.126609829981231,-6.13926343987081));
#5793=CARTESIAN_POINT('Ctrl Pts',(5.07259454704983,0.183954363014137,-6.13630498790999));
#5794=CARTESIAN_POINT('Ctrl Pts',(5.0646625579511,0.241019882873989,-6.13334653594918));
#5795=CARTESIAN_POINT('Ctrl Pts',(5.05358226242277,0.297424931821321,-6.13038808398836));
#5796=CARTESIAN_POINT('Ctrl Pts',(5.0424973401078,0.353853533761988,-6.12742839667006));
#5797=CARTESIAN_POINT('Ctrl Pts',(5.02826161926058,0.40962060716878,-6.12446870935177));
#5798=CARTESIAN_POINT('Ctrl Pts',(5.01098814647375,0.464357297097349,-6.12150902203347));
#5799=CARTESIAN_POINT('Ctrl Pts',(4.99368136679308,0.519199530893311,-6.11854362781462));
#5800=CARTESIAN_POINT('Ctrl Pts',(4.9733253157744,0.57300692032904,-6.11557823359577));
#5801=CARTESIAN_POINT('Ctrl Pts',(4.95008188101104,0.625429053501209,-6.11261283937692));
#5802=CARTESIAN_POINT('Ctrl Pts',(4.9290766905821,0.672803157250667,-6.10993300006324));
#5803=CARTESIAN_POINT('Ctrl Pts',(4.9057141893479,0.719045982025723,-6.10725316074956));
#5804=CARTESIAN_POINT('Ctrl Pts',(4.88014509712215,0.763918060338797,-6.10457332143588));
#5805=CARTESIAN_POINT('Ctrl Pts',(4.85179886425067,0.813663838173202,-6.10160241622841));
#5806=CARTESIAN_POINT('Ctrl Pts',(4.82062127632723,0.861932893587305,-6.09863151102094));
#5807=CARTESIAN_POINT('Ctrl Pts',(4.78679087939057,0.908384271475387,-6.09566060581347));
#5808=CARTESIAN_POINT('Ctrl Pts',(4.75302018267901,0.954753676996385,-6.09269494333815));
#5809=CARTESIAN_POINT('Ctrl Pts',(4.71660627330049,0.999311354084992,-6.08972928086283));
#5810=CARTESIAN_POINT('Ctrl Pts',(4.67777236989149,1.04174295328499,-6.08676361838751));
#5811=CARTESIAN_POINT('Ctrl Pts',(4.6389767606605,1.08413271061307,-6.08380088035699));
#5812=CARTESIAN_POINT('Ctrl Pts',(4.59776623569061,1.12440016161227,-6.08083814232647));
#5813=CARTESIAN_POINT('Ctrl Pts',(4.5544048047997,1.16226326861138,-6.07787540429594));
#5814=CARTESIAN_POINT('Ctrl Pts',(4.51106946267869,1.20010359495345,-6.0749144488217));
#5815=CARTESIAN_POINT('Ctrl Pts',(4.46558617173701,1.23554210300131,-6.07195349334745));
#5816=CARTESIAN_POINT('Ctrl Pts',(4.41825480438215,1.26833452791991,-6.0689925378732));
#5817=CARTESIAN_POINT('Ctrl Pts',(4.37093371915363,1.30111982910906,-6.06603222562816));
#5818=CARTESIAN_POINT('Ctrl Pts',(4.32176578271883,1.3312598919607,-6.06307191338313));
#5819=CARTESIAN_POINT('Ctrl Pts',(4.2710810612163,1.35855291555539,-6.06011160113809));
#5820=CARTESIAN_POINT('Ctrl Pts',(4.22035075106559,1.38587048800846,-6.05714862622413));
#5821=CARTESIAN_POINT('Ctrl Pts',(4.1681013890533,1.41033565572674,-6.05418565131016));
#5822=CARTESIAN_POINT('Ctrl Pts',(4.11468773232934,1.43179257832764,-6.05122267639619));
#5823=CARTESIAN_POINT('Ctrl Pts',(4.06125157419493,1.45325854002176,-6.04825845327869));
#5824=CARTESIAN_POINT('Ctrl Pts',(4.0066506377794,1.47171356196304,-6.04529423016119));
#5825=CARTESIAN_POINT('Ctrl Pts',(3.95125671194513,1.48705114171782,-6.0423300070437));
#5826=CARTESIAN_POINT('Ctrl Pts',(3.8957568288956,1.50241805911595,-6.03936011397553));
#5827=CARTESIAN_POINT('Ctrl Pts',(3.83946143611798,1.51465550703195,-6.03639022090737));
#5828=CARTESIAN_POINT('Ctrl Pts',(3.78275347878595,1.52370798149086,-6.0334203278392));
#5829=CARTESIAN_POINT('Ctrl Pts',(3.7322660360912,1.53176745509902,-6.03077621380048));
#5830=CARTESIAN_POINT('Ctrl Pts',(3.68145194585289,1.53730309517344,-6.02813209976177));
#5831=CARTESIAN_POINT('Ctrl Pts',(3.63058241961525,1.54031050856357,-6.02548798572305));
#5832=CARTESIAN_POINT('Ctrl Pts',(3.5734292076912,1.54368941431603,-6.02251725607048));
#5833=CARTESIAN_POINT('Ctrl Pts',(3.51596930837668,1.54389000739262,-6.01954652641792));
#5834=CARTESIAN_POINT('Ctrl Pts',(3.45858585276228,1.54087599031084,-6.01657579676535));
#5835=CARTESIAN_POINT('Ctrl Pts',(3.40130335532185,1.53786727597108,-6.01361029369661));
#5836=CARTESIAN_POINT('Ctrl Pts',(3.34409755080177,1.53165520442107,-6.01064479062787));
#5837=CARTESIAN_POINT('Ctrl Pts',(3.28735363447812,1.52225543290256,-6.00767928755913));
#5838=CARTESIAN_POINT('Ctrl Pts',(3.2306654857854,1.51286489943145,-6.00471669897165));
#5839=CARTESIAN_POINT('Ctrl Pts',(3.17443883741385,1.50029295806146,-6.00175411038417));
#5840=CARTESIAN_POINT('Ctrl Pts',(3.11905404576029,1.48460707928192,-5.99879152179669));
#5841=CARTESIAN_POINT('Ctrl Pts',(3.06370238715066,1.4689305843223,-5.99583070552928));
#5842=CARTESIAN_POINT('Ctrl Pts',(3.00919208724658,1.45014398657061,-5.99286988926187));
#5843=CARTESIAN_POINT('Ctrl Pts',(2.95589139740111,1.42836541635121,-5.98990907299446));
#5844=CARTESIAN_POINT('Ctrl Pts',(2.90260209758853,1.40659150007967,-5.98694888943546));
#5845=CARTESIAN_POINT('Ctrl Pts',(2.85052237671371,1.38182707787297,-5.98398870587646));
#5846=CARTESIAN_POINT('Ctrl Pts',(2.80000135672649,1.35423874583096,-5.98102852231746));
#5847=CARTESIAN_POINT('Ctrl Pts',(2.7494345918152,1.32662543356973,-5.9780656584212));
#5848=CARTESIAN_POINT('Ctrl Pts',(2.70042980679601,1.29618335169555,-5.97510279452494));
#5849=CARTESIAN_POINT('Ctrl Pts',(2.65331106399839,1.26312485716862,-5.97213993062869));
#5850=CARTESIAN_POINT('Ctrl Pts',(2.60617231945885,1.23005232942611,-5.96917580900704));
#5851=CARTESIAN_POINT('Ctrl Pts',(2.56092162380492,1.19436149745353,-5.9662116873854));
#5852=CARTESIAN_POINT('Ctrl Pts',(2.51785096846392,1.15630589824063,-5.96324756576375));
#5853=CARTESIAN_POINT('Ctrl Pts',(2.47469767089845,1.11817727948931,-5.96027775670591));
#5854=CARTESIAN_POINT('Ctrl Pts',(2.43373314442815,1.07767519380697,-5.95730794764806));
#5855=CARTESIAN_POINT('Ctrl Pts',(2.39521271537853,1.03509033981442,-5.95433813859021));
#5856=CARTESIAN_POINT('Ctrl Pts',(2.36090316675489,0.997160670941657,-5.95169297573022));
#5857=CARTESIAN_POINT('Ctrl Pts',(2.32853216646961,0.957579404572623,-5.94904781287022));
#5858=CARTESIAN_POINT('Ctrl Pts',(2.2982514595631,0.91657174726307,-5.94640265001023));
#5859=CARTESIAN_POINT('Ctrl Pts',(2.26409693031632,0.870317964772287,-5.94341909046048));
#5860=CARTESIAN_POINT('Ctrl Pts',(2.23245953901597,0.822055478003167,-5.94043553091072));
#5861=CARTESIAN_POINT('Ctrl Pts',(2.2035811354599,0.77208735733987,-5.93745197136097));
#5862=CARTESIAN_POINT('Ctrl Pts',(2.17474883426353,0.722199007300613,-5.93447317485622));
#5863=CARTESIAN_POINT('Ctrl Pts',(2.14866704348227,0.670610863712113,-5.93149437835146));
#5864=CARTESIAN_POINT('Ctrl Pts',(2.12553550006044,0.617656473538582,-5.9285155818467));
#5865=CARTESIAN_POINT('Ctrl Pts',(2.10243419074161,0.564771297444616,-5.92554067878039));
#5866=CARTESIAN_POINT('Ctrl Pts',(2.08227568039562,0.510523888301181,-5.92256577571407));
#5867=CARTESIAN_POINT('Ctrl Pts',(2.06521366265845,0.455272032534889,-5.91959087264776));
#5868=CARTESIAN_POINT('Ctrl Pts',(2.04816489876985,0.400063096647172,-5.91661828049891));
#5869=CARTESIAN_POINT('Ctrl Pts',(2.03420800733172,0.34385175250833,-5.91364568835005));
#5870=CARTESIAN_POINT('Ctrl Pts',(2.02344773952354,0.287013554153131,-5.9106730962012));
#5871=CARTESIAN_POINT('Ctrl Pts',(2.01268935513701,0.230185304462381,-5.90770102435952));
#5872=CARTESIAN_POINT('Ctrl Pts',(2.00512659039881,0.172730921831388,-5.90472895251783));
#5873=CARTESIAN_POINT('Ctrl Pts',(2.00081326718839,0.115037005526063,-5.90175688067614));
#5874=CARTESIAN_POINT('Ctrl Pts',(1.99792588528997,0.0764161182281746,-5.89976734592118));
#5875=CARTESIAN_POINT('Ctrl Pts',(1.99649355035822,0.037688117570368,-5.89777781116623));
#5876=CARTESIAN_POINT('Ctrl Pts',(1.99651939415621,-0.0010299323318173,
-5.89578827641127));
#5877=CARTESIAN_POINT('Ctrl Pts',(4.49572832313563,-0.823999039924152,-6.49872963456835));
#5878=CARTESIAN_POINT('Ctrl Pts',(4.76877456504554,-0.507155625959688,-6.47236100750229));
#5879=CARTESIAN_POINT('Ctrl Pts',(4.97052119895137,0.41371606398221,-6.41963060186529));
#5880=CARTESIAN_POINT('Ctrl Pts',(3.97155283172513,1.42700839004805,-6.34053841765734));
#5881=CARTESIAN_POINT('Ctrl Pts',(2.58001075957843,1.1395105179617,-6.26145308194453));
#5882=CARTESIAN_POINT('Ctrl Pts',(2.0606601689097,-0.182061886182395,-6.18236774623168));
#5883=CARTESIAN_POINT('Ctrl Pts',(2.88560714750128,-1.33903079709423,-6.10328241051888));
#5884=CARTESIAN_POINT('Ctrl Pts',(4.30496409563768,-1.27835189863699,-6.02419707480604));
#5885=CARTESIAN_POINT('Ctrl Pts',(5.02852611711507,-0.0558761027051249,
-5.94511173909324));
#5886=CARTESIAN_POINT('Ctrl Pts',(4.39856758010236,1.21751315736083,-5.8660264033804));
#5887=CARTESIAN_POINT('Ctrl Pts',(2.98772827969131,1.38410915310173,-5.78694106766758));
#5888=CARTESIAN_POINT('Ctrl Pts',(2.07846881472217,0.292573992443711,-5.70785573195475));
#5889=CARTESIAN_POINT('Ctrl Pts',(2.49732074732185,-1.06493663159316,-5.62877039624192));
#5890=CARTESIAN_POINT('Ctrl Pts',(3.86353027867868,-1.45438919355478,-5.5496850605291));
#5891=CARTESIAN_POINT('Ctrl Pts',(4.93522883507102,-0.521820717995012,-5.47059972481628));
#5892=CARTESIAN_POINT('Ctrl Pts',(4.73818094463292,0.885140580293045,-5.39151438910345));
#5893=CARTESIAN_POINT('Ctrl Pts',(3.45160733055285,1.48740082812334,-5.31242905339063));
#5894=CARTESIAN_POINT('Ctrl Pts',(2.2448142609951,0.737796557718971,-5.2333437176778));
#5895=CARTESIAN_POINT('Ctrl Pts',(2.21517534366209,-0.682849813790565,-5.15425838196498));
#5896=CARTESIAN_POINT('Ctrl Pts',(3.38887522286638,-1.48204143598075,-5.07517304625216));
#5897=CARTESIAN_POINT('Ctrl Pts',(4.70048975466964,-0.93549620915041,-4.99608771053934));
#5898=CARTESIAN_POINT('Ctrl Pts',(4.95482897497733,0.464382385782661,-4.91700237482651));
#5899=CARTESIAN_POINT('Ctrl Pts',(4.26949223942085,1.11144110680237,-4.86427881768463));
#5900=CARTESIAN_POINT('Ctrl Pts',(3.86552663736113,1.21943825288345,-4.83791703911368));
#5901=CARTESIAN_POINT('Ctrl Pts',(4.56709408744317,-0.885497419986959,-6.55312057472045));
#5902=CARTESIAN_POINT('Ctrl Pts',(4.86051887440726,-0.54500670093076,-6.52675194765439));
#5903=CARTESIAN_POINT('Ctrl Pts',(5.07732267533294,0.444593366634419,-6.47402154201738));
#5904=CARTESIAN_POINT('Ctrl Pts',(4.00379725968579,1.53351179608608,-6.39492935780944));
#5905=CARTESIAN_POINT('Ctrl Pts',(2.50839877620863,1.22455679535254,-6.31584402209662));
#5906=CARTESIAN_POINT('Ctrl Pts',(1.95028695104414,-0.195649900887397,-6.23675868638379));
#5907=CARTESIAN_POINT('Ctrl Pts',(2.83680305819412,-1.43896807964627,-6.15767335067098));
#5908=CARTESIAN_POINT('Ctrl Pts',(4.36209235432126,-1.37376046965137,-6.07858801495814));
#5909=CARTESIAN_POINT('Ctrl Pts',(5.13965673507314,-0.0600463621764277,
-5.99950267924533));
#5910=CARTESIAN_POINT('Ctrl Pts',(4.46268184530282,1.3083810871217,-5.92041734353249));
#5911=CARTESIAN_POINT('Ctrl Pts',(2.94654590339056,1.48741081563,-5.84133200781968));
#5912=CARTESIAN_POINT('Ctrl Pts',(1.96942472810011,0.314409972477684,-5.76224667210684));
#5913=CARTESIAN_POINT('Ctrl Pts',(2.41953727399302,-1.14441715831629,-5.68316133639403));
#5914=CARTESIAN_POINT('Ctrl Pts',(3.88771254673291,-1.56293613966857,-5.60407600068119));
#5915=CARTESIAN_POINT('Ctrl Pts',(5.03939629963695,-0.560766308080723,-5.52499066496838));
#5916=CARTESIAN_POINT('Ctrl Pts',(4.82764192840266,0.951202200729989,-5.44590532925554));
#5917=CARTESIAN_POINT('Ctrl Pts',(3.44504612344143,1.59841156600245,-5.36681999354273));
#5918=CARTESIAN_POINT('Ctrl Pts',(2.14818520762059,0.79286129798834,-5.28773465782989));
#5919=CARTESIAN_POINT('Ctrl Pts',(2.11633421804662,-0.733813656391856,-5.20864932211708));
#5920=CARTESIAN_POINT('Ctrl Pts',(3.37763206491069,-1.59265218075439,-5.12956398640425));
#5921=CARTESIAN_POINT('Ctrl Pts',(4.78713769253389,-1.00531607377421,-5.05047865069143));
#5922=CARTESIAN_POINT('Ctrl Pts',(5.06045927723462,0.499041120892308,-4.9713933149786));
#5923=CARTESIAN_POINT('Ctrl Pts',(4.32397309004998,1.19439245054404,-4.91866975783672));
#5924=CARTESIAN_POINT('Ctrl Pts',(3.88985790173582,1.31044986030698,-4.89230797926578));
#5925=CARTESIAN_POINT('Ctrl Pts',(4.63845985175071,-0.946995800049766,-6.60751151487254));
#5926=CARTESIAN_POINT('Ctrl Pts',(4.95226318376898,-0.58285777590183,-6.58114288780649));
#5927=CARTESIAN_POINT('Ctrl Pts',(5.18412415171451,0.475470669286626,-6.52841248216948));
#5928=CARTESIAN_POINT('Ctrl Pts',(4.03604168764646,1.64001520212411,-6.44932029796154));
#5929=CARTESIAN_POINT('Ctrl Pts',(2.43678679283885,1.30960307274338,-6.37023496224872));
#5930=CARTESIAN_POINT('Ctrl Pts',(1.83991373317858,-0.209237915592398,-6.29114962653589));
#5931=CARTESIAN_POINT('Ctrl Pts',(2.78799896888696,-1.53890536219829,-6.21206429082307));
#5932=CARTESIAN_POINT('Ctrl Pts',(4.41922061300483,-1.46916904066575,-6.13297895511024));
#5933=CARTESIAN_POINT('Ctrl Pts',(5.25078735303124,-0.0642166216477319,
-6.05389361939743));
#5934=CARTESIAN_POINT('Ctrl Pts',(4.52679611050327,1.39924901688256,-5.97480828368459));
#5935=CARTESIAN_POINT('Ctrl Pts',(2.90536352708983,1.59071247815826,-5.89572294797179));
#5936=CARTESIAN_POINT('Ctrl Pts',(1.86038064147805,0.336245952511657,-5.81663761225893));
#5937=CARTESIAN_POINT('Ctrl Pts',(2.34175380066418,-1.22389768503941,-5.73755227654613));
#5938=CARTESIAN_POINT('Ctrl Pts',(3.91189481478717,-1.67148308578238,-5.6584669408333));
#5939=CARTESIAN_POINT('Ctrl Pts',(5.14356376420288,-0.599711898166432,-5.57938160512047));
#5940=CARTESIAN_POINT('Ctrl Pts',(4.91710291217238,1.01726382116693,-5.50029626940765));
#5941=CARTESIAN_POINT('Ctrl Pts',(3.43848491633001,1.70942230388156,-5.42121093369482));
#5942=CARTESIAN_POINT('Ctrl Pts',(2.05155615424608,0.847926038257708,-5.34212559798201));
#5943=CARTESIAN_POINT('Ctrl Pts',(2.01749309243115,-0.784777498993147,-5.26304026226917));
#5944=CARTESIAN_POINT('Ctrl Pts',(3.36638890695502,-1.70326292552803,-5.18395492655636));
#5945=CARTESIAN_POINT('Ctrl Pts',(4.87378563039813,-1.07513593839801,-5.10486959084353));
#5946=CARTESIAN_POINT('Ctrl Pts',(5.16608957949192,0.533699856001957,-5.0257842551307));
#5947=CARTESIAN_POINT('Ctrl Pts',(4.3784539406791,1.27734379428573,-4.97306069798882));
#5948=CARTESIAN_POINT('Ctrl Pts',(3.91418916611049,1.40146146773053,-4.94669891941788));
#5949=CARTESIAN_POINT('Ctrl Pts',(4.70982561605824,-1.00849418011257,-6.66190245502464));
#5950=CARTESIAN_POINT('Ctrl Pts',(5.0440074931307,-0.620708850872902,-6.63553382795858));
#5951=CARTESIAN_POINT('Ctrl Pts',(5.29092562809607,0.506347971938834,-6.58280342232159));
#5952=CARTESIAN_POINT('Ctrl Pts',(4.06828611560712,1.74651860816213,-6.50371123811363));
#5953=CARTESIAN_POINT('Ctrl Pts',(2.36517480946905,1.39464935013422,-6.42462590240083));
#5954=CARTESIAN_POINT('Ctrl Pts',(1.72954051531302,-0.2228259302974,-6.34554056668798));
#5955=CARTESIAN_POINT('Ctrl Pts',(2.7391948795798,-1.63884264475033,-6.26645523097519));
#5956=CARTESIAN_POINT('Ctrl Pts',(4.47634887168841,-1.56457761168014,-6.18736989526234));
#5957=CARTESIAN_POINT('Ctrl Pts',(5.36191797098931,-0.0683868811190347,
-6.10828455954952));
#5958=CARTESIAN_POINT('Ctrl Pts',(4.59091037570374,1.49011694664342,-6.0291992238367));
#5959=CARTESIAN_POINT('Ctrl Pts',(2.86418115078907,1.69401414068653,-5.95011388812387));
#5960=CARTESIAN_POINT('Ctrl Pts',(1.75133655485599,0.358081932545629,-5.87102855241105));
#5961=CARTESIAN_POINT('Ctrl Pts',(2.26397032733535,-1.30337821176254,-5.79194321669822));
#5962=CARTESIAN_POINT('Ctrl Pts',(3.93607708284141,-1.78003003189618,-5.71285788098541));
#5963=CARTESIAN_POINT('Ctrl Pts',(5.24773122876883,-0.638657488252143,-5.63377254527257));
#5964=CARTESIAN_POINT('Ctrl Pts',(5.00656389594211,1.08332544160388,-5.55468720955976));
#5965=CARTESIAN_POINT('Ctrl Pts',(3.43192370921861,1.82043304176068,-5.47560187384691));
#5966=CARTESIAN_POINT('Ctrl Pts',(1.95492710087157,0.902990778527077,-5.39651653813412));
#5967=CARTESIAN_POINT('Ctrl Pts',(1.91865196681568,-0.835741341594439,-5.31743120242126));
#5968=CARTESIAN_POINT('Ctrl Pts',(3.35514574899934,-1.81387367030167,-5.23834586670847));
#5969=CARTESIAN_POINT('Ctrl Pts',(4.96043356826237,-1.14495580302182,-5.15926053099562));
#5970=CARTESIAN_POINT('Ctrl Pts',(5.27171988174921,0.568358591111605,-5.08017519528281));
#5971=CARTESIAN_POINT('Ctrl Pts',(4.43293479130822,1.3602951380274,-5.02745163814092));
#5972=CARTESIAN_POINT('Ctrl Pts',(3.93852043048518,1.49247307515406,-5.00108985956998));
#5973=CARTESIAN_POINT('',(4.49856554501718,-0.825828034651814,-4.99935673527973));
#5974=CARTESIAN_POINT('Ctrl Pts',(3.93803289228021,1.49064942821852,-5.));
#5975=CARTESIAN_POINT('Ctrl Pts',(3.99409065643514,1.47016615192376,-5.));
#5976=CARTESIAN_POINT('Ctrl Pts',(4.04865786654016,1.44624046411167,-5.));
#5977=CARTESIAN_POINT('Ctrl Pts',(4.10155167689883,1.41915239541907,-5.));
#5978=CARTESIAN_POINT('Ctrl Pts',(4.15531048656907,1.39162134179853,-5.));
#5979=CARTESIAN_POINT('Ctrl Pts',(4.20734148705644,1.36082280343506,-5.));
#5980=CARTESIAN_POINT('Ctrl Pts',(4.25742159252753,1.32700667838438,-5.));
#5981=CARTESIAN_POINT('Ctrl Pts',(4.30733738857824,1.29330150174034,-5.));
#5982=CARTESIAN_POINT('Ctrl Pts',(4.35531573175224,1.2565975723992,-5.));
#5983=CARTESIAN_POINT('Ctrl Pts',(4.40109443402577,1.21711234501117,-5.));
#5984=CARTESIAN_POINT('Ctrl Pts',(4.41061728847052,1.20889865492255,-5.));
#5985=CARTESIAN_POINT('Ctrl Pts',(4.42004479737223,1.20056453633304,-5.));
#5986=CARTESIAN_POINT('Ctrl Pts',(4.42937433420408,1.19211184027005,-5.));
#5987=CARTESIAN_POINT('Ctrl Pts',(4.43709254019515,1.18511903338479,-5.));
#5988=CARTESIAN_POINT('Ctrl Pts',(4.44474353367624,1.17804508607658,-5.));
#5989=CARTESIAN_POINT('Ctrl Pts',(4.4523156979883,1.17090094418241,-5.));
#5990=CARTESIAN_POINT('Ctrl Pts',(4.49538755285076,1.13026375907898,-5.));
#5991=CARTESIAN_POINT('Ctrl Pts',(4.53599880545883,1.08728056038843,-5.));
#5992=CARTESIAN_POINT('Ctrl Pts',(4.57394274742331,1.0421920409728,-5.));
#5993=CARTESIAN_POINT('Ctrl Pts',(4.61123044145062,0.997883336366205,-5.));
#5994=CARTESIAN_POINT('Ctrl Pts',(4.64594276168599,0.951540565975969,-5.));
#5995=CARTESIAN_POINT('Ctrl Pts',(4.67784006477363,0.903368830373567,-5.));
#5996=CARTESIAN_POINT('Ctrl Pts',(4.70128120204354,0.867967709981565,-5.));
#5997=CARTESIAN_POINT('Ctrl Pts',(4.72320117972997,0.831578293288047,-5.));
#5998=CARTESIAN_POINT('Ctrl Pts',(4.74348727685767,0.794278015648549,-5.));
#5999=CARTESIAN_POINT('Ctrl Pts',(4.75387319409623,0.77518131143282,-5.));
#6000=CARTESIAN_POINT('Ctrl Pts',(4.76383059074213,0.755845823276845,-5.));
#6001=CARTESIAN_POINT('Ctrl Pts',(4.77334264614643,0.736281858177808,-5.));
#6002=CARTESIAN_POINT('Ctrl Pts',(4.77823393014549,0.72622168659768,-5.));
#6003=CARTESIAN_POINT('Ctrl Pts',(4.78300365060887,0.716108772548597,-5.));
#6004=CARTESIAN_POINT('Ctrl Pts',(4.78764749050887,0.705950521112731,-5.));
#6005=CARTESIAN_POINT('Ctrl Pts',(4.81080973037988,0.655283861302306,-5.));
#6006=CARTESIAN_POINT('Ctrl Pts',(4.83086651830312,0.603444698612965,-5.));
#6007=CARTESIAN_POINT('Ctrl Pts',(4.84760491848966,0.550623118129289,-5.));
#6008=CARTESIAN_POINT('Ctrl Pts',(4.8593983757285,0.513406356444801,-5.));
#6009=CARTESIAN_POINT('Ctrl Pts',(4.86954356797092,0.475701506087563,-5.));
#6010=CARTESIAN_POINT('Ctrl Pts',(4.87795053537239,0.437572846428279,-5.));
#6011=CARTESIAN_POINT('Ctrl Pts',(4.88985018734038,0.383603589943183,-5.));
#6012=CARTESIAN_POINT('Ctrl Pts',(4.89826878476809,0.328784212898911,-5.));
#6013=CARTESIAN_POINT('Ctrl Pts',(4.9032634076361,0.273432028782955,-5.));
#6014=CARTESIAN_POINT('Ctrl Pts',(4.90468835253674,0.257640283424103,-5.));
#6015=CARTESIAN_POINT('Ctrl Pts',(4.90583433078692,0.241805257431463,-5.));
#6016=CARTESIAN_POINT('Ctrl Pts',(4.90670202416689,0.225934580336756,-5.));
#6017=CARTESIAN_POINT('Ctrl Pts',(4.90737234904755,0.213673901651028,-5.));
#6018=CARTESIAN_POINT('Ctrl Pts',(4.90787651819931,0.201389247372144,-5.));
#6019=CARTESIAN_POINT('Ctrl Pts',(4.90821450591308,0.189107888094874,-5.));
#6020=CARTESIAN_POINT('Ctrl Pts',(4.90974223500557,0.133595249324311,-5.));
#6021=CARTESIAN_POINT('Ctrl Pts',(4.907886088605,0.078048827692731,-5.));
#6022=CARTESIAN_POINT('Ctrl Pts',(4.9027539571184,0.0227840637894804,-5.));
#6023=CARTESIAN_POINT('Ctrl Pts',(4.89762247605141,-0.0324736961456407,
-5.));
#6024=CARTESIAN_POINT('Ctrl Pts',(4.88921538506426,-0.0874510038276154,
-5.));
#6025=CARTESIAN_POINT('Ctrl Pts',(4.87759161308525,-0.14181744386592,-5.));
#6026=CARTESIAN_POINT('Ctrl Pts',(4.87038507021592,-0.175523721096468,-5.));
#6027=CARTESIAN_POINT('Ctrl Pts',(4.86194116529405,-0.208994828372916,-5.));
#6028=CARTESIAN_POINT('Ctrl Pts',(4.85226563868636,-0.242146239785466,-5.));
#6029=CARTESIAN_POINT('Ctrl Pts',(4.84728116924316,-0.259224607081082,-5.));
#6030=CARTESIAN_POINT('Ctrl Pts',(4.84196973886336,-0.276218043618959,-5.));
#6031=CARTESIAN_POINT('Ctrl Pts',(4.83633153787352,-0.293114371811587,-5.));
#6032=CARTESIAN_POINT('Ctrl Pts',(4.83137886705509,-0.307956331459553,-5.00000000000001));
#6033=CARTESIAN_POINT('Ctrl Pts',(4.82617357016375,-0.322723784665042,-5.));
#6034=CARTESIAN_POINT('Ctrl Pts',(4.82072625926819,-0.33738190195413,-5.));
#6035=CARTESIAN_POINT('Ctrl Pts',(4.8020408199964,-0.38766237349243,-5.));
#6036=CARTESIAN_POINT('Ctrl Pts',(4.78048542226647,-0.436737790266667,-5.));
#6037=CARTESIAN_POINT('Ctrl Pts',(4.75610356324102,-0.484292455085576,-5.));
#6038=CARTESIAN_POINT('Ctrl Pts',(4.74073117822194,-0.514274935760493,-5.));
#6039=CARTESIAN_POINT('Ctrl Pts',(4.72423443746592,-0.543652342157504,-5.));
#6040=CARTESIAN_POINT('Ctrl Pts',(4.70661689619086,-0.572337713302352,-5.));
#6041=CARTESIAN_POINT('Ctrl Pts',(4.69812236738934,-0.586168741569455,-5.));
#6042=CARTESIAN_POINT('Ctrl Pts',(4.68936481385441,-0.599841995803325,-5.));
#6043=CARTESIAN_POINT('Ctrl Pts',(4.68035979413337,-0.613324827934156,-5.));
#6044=CARTESIAN_POINT('Ctrl Pts',(4.65190463621292,-0.655929522802452,-5.));
#6045=CARTESIAN_POINT('Ctrl Pts',(4.62095551630975,-0.696679989535698,-5.));
#6046=CARTESIAN_POINT('Ctrl Pts',(4.58753688857224,-0.735275095170701,-5.));
#6047=CARTESIAN_POINT('Ctrl Pts',(4.56897483790831,-0.756712369968577,-5.));
#6048=CARTESIAN_POINT('Ctrl Pts',(4.54965034106223,-0.777484018727688,-5.));
#6049=CARTESIAN_POINT('Ctrl Pts',(4.52956373601773,-0.797532559017432,-5.));
#6050=CARTESIAN_POINT('Ctrl Pts',(4.51970691265084,-0.807370703390872,-5.));
#6051=CARTESIAN_POINT('Ctrl Pts',(4.50966652692015,-0.817034646361409,-5.));
#6052=CARTESIAN_POINT('Ctrl Pts',(4.49944832123852,-0.826521983932989,-5.));
#6053=CARTESIAN_POINT('Ctrl Pts',(4.4976352031454,-0.825211298936469,-6.5));
#6054=CARTESIAN_POINT('Ctrl Pts',(4.53473403611661,-0.790565919373912,-6.5));
#6055=CARTESIAN_POINT('Ctrl Pts',(4.56942439597947,-0.753655314382007,-6.5));
#6056=CARTESIAN_POINT('Ctrl Pts',(4.60170505482589,-0.714805016616039,-6.5));
#6057=CARTESIAN_POINT('Ctrl Pts',(4.63521429205091,-0.674476104796233,-6.5));
#6058=CARTESIAN_POINT('Ctrl Pts',(4.66612750740978,-0.632056529770239,-6.5));
#6059=CARTESIAN_POINT('Ctrl Pts',(4.69441520294597,-0.587860718560562,-6.5));
#6060=CARTESIAN_POINT('Ctrl Pts',(4.71720257347233,-0.552258443201673,-6.5));
#6061=CARTESIAN_POINT('Ctrl Pts',(4.73828573819916,-0.515502374121504,-6.5));
#6062=CARTESIAN_POINT('Ctrl Pts',(4.75763279341486,-0.477738744113682,-6.5));
#6063=CARTESIAN_POINT('Ctrl Pts',(4.76647244363112,-0.460484579257903,-6.5));
#6064=CARTESIAN_POINT('Ctrl Pts',(4.77494945031063,-0.443019888823993,-6.5));
#6065=CARTESIAN_POINT('Ctrl Pts',(4.78305959925634,-0.425357785247147,-6.5));
#6066=CARTESIAN_POINT('Ctrl Pts',(4.78684697504658,-0.417109721748024,-6.5));
#6067=CARTESIAN_POINT('Ctrl Pts',(4.79055297375982,-0.408821425564243,-6.5));
#6068=CARTESIAN_POINT('Ctrl Pts',(4.7941739531994,-0.40050235122582,-6.5));
#6069=CARTESIAN_POINT('Ctrl Pts',(4.81595160644151,-0.350468950246823,-6.5));
#6070=CARTESIAN_POINT('Ctrl Pts',(4.83469510425185,-0.299242701997503,-6.5));
#6071=CARTESIAN_POINT('Ctrl Pts',(4.85037713536496,-0.247156898168492,-6.5));
#6072=CARTESIAN_POINT('Ctrl Pts',(4.86632338221363,-0.194193536523689,-6.5));
#6073=CARTESIAN_POINT('Ctrl Pts',(4.87910472028871,-0.14034047034307,-6.5));
#6074=CARTESIAN_POINT('Ctrl Pts',(4.88865141719124,-0.0859136452486175,
-6.5));
#6075=CARTESIAN_POINT('Ctrl Pts',(4.89555760061471,-0.0465406934206672,
-6.5));
#6076=CARTESIAN_POINT('Ctrl Pts',(4.90077019034692,-0.00686669826656089,
-6.5));
#6077=CARTESIAN_POINT('Ctrl Pts',(4.90424708276949,0.0329952762835868,-6.5));
#6078=CARTESIAN_POINT('Ctrl Pts',(4.90544059215015,0.0466786563756833,-6.5));
#6079=CARTESIAN_POINT('Ctrl Pts',(4.9064294554003,0.060384216236401,-6.5));
#6080=CARTESIAN_POINT('Ctrl Pts',(4.90721157306747,0.0741074501673721,-6.5));
#6081=CARTESIAN_POINT('Ctrl Pts',(4.90776877420489,0.0838842419165997,-6.5));
#6082=CARTESIAN_POINT('Ctrl Pts',(4.90822089056527,0.0936690684444187,-6.5));
#6083=CARTESIAN_POINT('Ctrl Pts',(4.90856697997868,0.103447389902126,-6.5));
#6084=CARTESIAN_POINT('Ctrl Pts',(4.91057764169525,0.16025610997759,-6.5));
#6085=CARTESIAN_POINT('Ctrl Pts',(4.90902053110958,0.216957470431213,-6.49999999999999));
#6086=CARTESIAN_POINT('Ctrl Pts',(4.90383821984126,0.273218400759099,-6.5));
#6087=CARTESIAN_POINT('Ctrl Pts',(4.90018706316735,0.312856597040903,-6.5));
#6088=CARTESIAN_POINT('Ctrl Pts',(4.89473554441125,0.352276864102268,-6.5));
#6089=CARTESIAN_POINT('Ctrl Pts',(4.88744880947781,0.39136760658551,-6.5));
#6090=CARTESIAN_POINT('Ctrl Pts',(4.87737256927013,0.445423053195733,-6.5));
#6091=CARTESIAN_POINT('Ctrl Pts',(4.86378936361766,0.498849002961625,-6.5));
#6092=CARTESIAN_POINT('Ctrl Pts',(4.8469261375644,0.551442578692384,-6.5));
#6093=CARTESIAN_POINT('Ctrl Pts',(4.84228985765719,0.565902358667974,-6.5));
#6094=CARTESIAN_POINT('Ctrl Pts',(4.83740534317848,0.580299187094379,-6.5));
#6095=CARTESIAN_POINT('Ctrl Pts',(4.83227664561688,0.594628735492603,-6.5));
#6096=CARTESIAN_POINT('Ctrl Pts',(4.8279040034594,0.606845869895838,-6.5));
#6097=CARTESIAN_POINT('Ctrl Pts',(4.82335243093813,0.619017360734909,-6.5));
#6098=CARTESIAN_POINT('Ctrl Pts',(4.81863426849385,0.631116085607377,-6.5));
#6099=CARTESIAN_POINT('Ctrl Pts',(4.79819471062682,0.68352898789047,-6.5));
#6100=CARTESIAN_POINT('Ctrl Pts',(4.77460300293305,0.734665692265129,-6.5));
#6101=CARTESIAN_POINT('Ctrl Pts',(4.7481393208072,0.784323343086663,-6.5));
#6102=CARTESIAN_POINT('Ctrl Pts',(4.72080038497767,0.835623359569603,-6.5));
#6103=CARTESIAN_POINT('Ctrl Pts',(4.69039609513946,0.885345769139235,-6.5));
#6104=CARTESIAN_POINT('Ctrl Pts',(4.65717979150465,0.933261327103311,-6.5));
#6105=CARTESIAN_POINT('Ctrl Pts',(4.63626695867212,0.963428743225127,-6.5));
#6106=CARTESIAN_POINT('Ctrl Pts',(4.61423837261579,0.9928797854586,-6.5));
#6107=CARTESIAN_POINT('Ctrl Pts',(4.59114735991414,1.02155360927412,-6.5));
#6108=CARTESIAN_POINT('Ctrl Pts',(4.58004021989682,1.03534616917896,-6.5));
#6109=CARTESIAN_POINT('Ctrl Pts',(4.56868715418712,1.04895884536489,-6.5));
#6110=CARTESIAN_POINT('Ctrl Pts',(4.55709354204463,1.0623845162606,-6.5));
#6111=CARTESIAN_POINT('Ctrl Pts',(4.54985583002559,1.07076595410856,-6.5));
#6112=CARTESIAN_POINT('Ctrl Pts',(4.54252436265672,1.07907450530581,-6.5));
#6113=CARTESIAN_POINT('Ctrl Pts',(4.53510038293429,1.0873083833382,-6.5));
#6114=CARTESIAN_POINT('Ctrl Pts',(4.52747285907183,1.09576801058945,-6.5));
#6115=CARTESIAN_POINT('Ctrl Pts',(4.51975341789829,1.10414241451658,-6.5));
#6116=CARTESIAN_POINT('Ctrl Pts',(4.51194611870614,1.11242760866335,-6.5));
#6117=CARTESIAN_POINT('Ctrl Pts',(4.47050176490355,1.15640882535441,-6.5));
#6118=CARTESIAN_POINT('Ctrl Pts',(4.42656593670862,1.19789966714169,-6.5));
#6119=CARTESIAN_POINT('Ctrl Pts',(4.3803955573361,1.23664844871276,-6.5));
#6120=CARTESIAN_POINT('Ctrl Pts',(4.34807267706821,1.26377562947823,-6.5));
#6121=CARTESIAN_POINT('Ctrl Pts',(4.31465351835422,1.28955859641289,-6.5));
#6122=CARTESIAN_POINT('Ctrl Pts',(4.28021363858723,1.3139024861197,-6.5));
#6123=CARTESIAN_POINT('Ctrl Pts',(4.26678858690377,1.32339200756117,-6.5));
#6124=CARTESIAN_POINT('Ctrl Pts',(4.25320628510412,1.33266389379897,-6.5));
#6125=CARTESIAN_POINT('Ctrl Pts',(4.23949101849253,1.34169951148356,-6.5));
#6126=CARTESIAN_POINT('Ctrl Pts',(4.18870128727318,1.37515978656226,-6.5));
#6127=CARTESIAN_POINT('Ctrl Pts',(4.13603515427771,1.40542369855342,-6.5));
#6128=CARTESIAN_POINT('Ctrl Pts',(4.08173184346464,1.4322271097713,-6.5));
#6129=CARTESIAN_POINT('Ctrl Pts',(4.05045913624191,1.44766291320642,-6.5));
#6130=CARTESIAN_POINT('Ctrl Pts',(4.01864270350732,1.46195048487063,-6.5));
#6131=CARTESIAN_POINT('Ctrl Pts',(3.98632298496835,1.47503347997995,-6.5));
#6132=CARTESIAN_POINT('Ctrl Pts',(3.97074861183692,1.48133797323423,-6.5));
#6133=CARTESIAN_POINT('Ctrl Pts',(3.9550573186525,1.48736267540842,-6.5));
#6134=CARTESIAN_POINT('Ctrl Pts',(3.93925596516474,1.49310957330526,-6.49999999999999));
#6135=CARTESIAN_POINT('Ctrl Pts',(4.49772637506564,-0.825105431445688,-4.99935673527973));
#6136=CARTESIAN_POINT('Ctrl Pts',(4.49344280469424,-0.830080006026179,-4.99957115685316));
#6137=CARTESIAN_POINT('Ctrl Pts',(4.48912049496684,-0.835021222417506,-4.99978557842658));
#6138=CARTESIAN_POINT('Ctrl Pts',(4.48475997009368,-0.83992848134833,-5.));
#6139=CARTESIAN_POINT('Ctrl Pts',(3.14049567003405,1.49255536784005,-6.49886096014758));
#6140=CARTESIAN_POINT('Ctrl Pts',(2.64605404795825,1.36037014262379,-6.47249918157664));
#6141=CARTESIAN_POINT('Ctrl Pts',(1.80722122039271,0.568399038714978,-6.41977562443476));
#6142=CARTESIAN_POINT('Ctrl Pts',(2.11852749381716,-1.14502364307201,-6.34069028872192));
#6143=CARTESIAN_POINT('Ctrl Pts',(3.72390230442703,-1.8139700754625,-6.26160495300911));
#6144=CARTESIAN_POINT('Ctrl Pts',(5.16047486326952,-0.835788897306109,-6.18251961729628));
#6145=CARTESIAN_POINT('Ctrl Pts',(5.12419795286652,0.903041288099895,-6.10343428158346));
#6146=CARTESIAN_POINT('Ctrl Pts',(3.64712017679401,1.82053219154147,-6.02434894587063));
#6147=CARTESIAN_POINT('Ctrl Pts',(2.07239390111447,1.08338514516621,-5.9452636101578));
#6148=CARTESIAN_POINT('Ctrl Pts',(1.83121321908415,-0.638692684208562,-5.86617827444498));
#6149=CARTESIAN_POINT('Ctrl Pts',(3.14293932672556,-1.78012743927191,-5.78709293873216));
#6150=CARTESIAN_POINT('Ctrl Pts',(4.81513763610179,-1.3034497215919,-5.70800760301933));
#6151=CARTESIAN_POINT('Ctrl Pts',(5.32779955515347,0.35810164653081,-5.62892226730652));
#6152=CARTESIAN_POINT('Ctrl Pts',(4.21489391379536,1.69410683583459,-5.54983693159369));
#6153=CARTESIAN_POINT('Ctrl Pts',(2.48807018469715,1.4901987924474,-5.47075159588087));
#6154=CARTESIAN_POINT('Ctrl Pts',(1.71702014690403,-0.0683909582657119,
-5.39166626016802));
#6155=CARTESIAN_POINT('Ctrl Pts',(2.60263814280788,-1.56466278404689,-5.31258092445522));
#6156=CARTESIAN_POINT('Ctrl Pts',(4.3398865979832,-1.63893336675877,-5.2334955887424));
#6157=CARTESIAN_POINT('Ctrl Pts',(5.34959768449681,-0.222836636419013,-5.15441025302956));
#6158=CARTESIAN_POINT('Ctrl Pts',(4.7139258330361,1.39472338762311,-5.07532491731675));
#6159=CARTESIAN_POINT('Ctrl Pts',(3.01072656391766,1.74661806167074,-4.99623958160391));
#6160=CARTESIAN_POINT('Ctrl Pts',(1.7881154138621,0.506476594702042,-4.9171542458911));
#6161=CARTESIAN_POINT('Ctrl Pts',(2.03488352866203,-0.620450306009015,-4.86443068874921));
#6162=CARTESIAN_POINT('Ctrl Pts',(2.36888760166378,-1.0082475863304,-4.83806891017827));
#6163=CARTESIAN_POINT('Ctrl Pts',(3.16479427350219,1.40166592922615,-6.55317888899264));
#6164=CARTESIAN_POINT('Ctrl Pts',(2.70046176658963,1.27753014805185,-6.5268171104217));
#6165=CARTESIAN_POINT('Ctrl Pts',(1.9127098211348,0.533786272816551,-6.47409355327982));
#6166=CARTESIAN_POINT('Ctrl Pts',(2.20505904074524,-1.07529721391509,-6.39500821756699));
#6167=CARTESIAN_POINT('Ctrl Pts',(3.71267425164766,-1.70350802804124,-6.31592288185417));
#6168=CARTESIAN_POINT('Ctrl Pts',(5.06176645551324,-0.784893375898539,-6.23683754614134));
#6169=CARTESIAN_POINT('Ctrl Pts',(5.0276986343623,0.848050419761554,-6.15775221042852));
#6170=CARTESIAN_POINT('Ctrl Pts',(3.64056778605475,1.70967054283278,-6.0786668747157));
#6171=CARTESIAN_POINT('Ctrl Pts',(2.16173476180896,1.01741220388143,-5.99958153900286));
#6172=CARTESIAN_POINT('Ctrl Pts',(1.93524082257328,-0.599799373604929,-5.92049620329005));
#6173=CARTESIAN_POINT('Ctrl Pts',(3.16708912326188,-1.6717262455187,-5.84141086757722));
#6174=CARTESIAN_POINT('Ctrl Pts',(4.7374586034602,-1.22407590671736,-5.7623255318644));
#6175=CARTESIAN_POINT('Ctrl Pts',(5.21890187895245,0.336294979708794,-5.68324019615157));
#6176=CARTESIAN_POINT('Ctrl Pts',(4.1737668350226,1.59094388283553,-5.60415486043875));
#6177=CARTESIAN_POINT('Ctrl Pts',(2.55209836026517,1.39945285793332,-5.52506952472592));
#6178=CARTESIAN_POINT('Ctrl Pts',(1.82800155890686,-0.064226278055535,-5.4459841890131));
#6179=CARTESIAN_POINT('Ctrl Pts',(2.65968968111326,-1.46938235082056,-5.36689885330027));
#6180=CARTESIAN_POINT('Ctrl Pts',(4.29114806630124,-1.53913021249062,-5.28781351758746));
#6181=CARTESIAN_POINT('Ctrl Pts',(5.23937260712761,-0.209266957716878,-5.20872818187462));
#6182=CARTESIAN_POINT('Ctrl Pts',(4.64241011209466,1.30979144576409,-5.12964284616181));
#6183=CARTESIAN_POINT('Ctrl Pts',(3.04292748140275,1.64025742774137,-5.05055751044898));
#6184=CARTESIAN_POINT('Ctrl Pts',(1.89476746627053,0.475634607627104,-4.97147217473615));
#6185=CARTESIAN_POINT('Ctrl Pts',(2.12650859051101,-0.58266786844183,-4.91874861759427));
#6186=CARTESIAN_POINT('Ctrl Pts',(2.44017342294322,-0.946850160760849,-4.89238683902333));
#6187=CARTESIAN_POINT('Ctrl Pts',(3.18909287697032,1.31077649061224,-6.6074968178377));
#6188=CARTESIAN_POINT('Ctrl Pts',(2.754869485221,1.19469015347991,-6.58113503926676));
#6189=CARTESIAN_POINT('Ctrl Pts',(2.01819842187689,0.499173506918126,-6.52841148212487));
#6190=CARTESIAN_POINT('Ctrl Pts',(2.29159058767332,-1.00557078475819,-6.44932614641205));
#6191=CARTESIAN_POINT('Ctrl Pts',(3.7014461988683,-1.59304598061997,-6.37024081069922));
#6192=CARTESIAN_POINT('Ctrl Pts',(4.96305804775698,-0.733997854490971,-6.29115547498641));
#6193=CARTESIAN_POINT('Ctrl Pts',(4.93119931585807,0.793059551423215,-6.21207013927357));
#6194=CARTESIAN_POINT('Ctrl Pts',(3.63401539531548,1.5988088941241,-6.13298480356076));
#6195=CARTESIAN_POINT('Ctrl Pts',(2.25107562250343,0.951439262596645,-6.05389946784793));
#6196=CARTESIAN_POINT('Ctrl Pts',(2.03926842606242,-0.560906063001296,-5.9748141321351));
#6197=CARTESIAN_POINT('Ctrl Pts',(3.19123891979818,-1.56332505176548,-5.89572879642229));
#6198=CARTESIAN_POINT('Ctrl Pts',(4.65977957081863,-1.14470209184282,-5.81664346070945));
#6199=CARTESIAN_POINT('Ctrl Pts',(5.11000420275143,0.314488312886777,-5.73755812499664));
#6200=CARTESIAN_POINT('Ctrl Pts',(4.13263975624985,1.48778092983647,-5.65847278928381));
#6201=CARTESIAN_POINT('Ctrl Pts',(2.61612653583318,1.30870692341923,-5.57938745357099));
#6202=CARTESIAN_POINT('Ctrl Pts',(1.93898297090969,-0.0600615978453574,
-5.50030211785817));
#6203=CARTESIAN_POINT('Ctrl Pts',(2.71674121941864,-1.37410191759422,-5.42121678214533));
#6204=CARTESIAN_POINT('Ctrl Pts',(4.24240953461929,-1.43932705822246,-5.34213144643252));
#6205=CARTESIAN_POINT('Ctrl Pts',(5.12914752975841,-0.195697279014745,-5.26304611071968));
#6206=CARTESIAN_POINT('Ctrl Pts',(4.57089439115325,1.22485950390509,-5.18396077500686));
#6207=CARTESIAN_POINT('Ctrl Pts',(3.07512839888781,1.53389679381199,-5.10487543929403));
#6208=CARTESIAN_POINT('Ctrl Pts',(2.00141951867897,0.444792620552168,-5.02579010358122));
#6209=CARTESIAN_POINT('Ctrl Pts',(2.21813365236001,-0.544885430874644,-4.97306654643933));
#6210=CARTESIAN_POINT('Ctrl Pts',(2.51145924422265,-0.885452735191297,-4.94670476786839));
#6211=CARTESIAN_POINT('Ctrl Pts',(3.21339148043844,1.21988705199834,-6.66181474668277));
#6212=CARTESIAN_POINT('Ctrl Pts',(2.80927720385237,1.11185015890796,-6.63545296811183));
#6213=CARTESIAN_POINT('Ctrl Pts',(2.12368702261897,0.4645607410197,-6.58272941096994));
#6214=CARTESIAN_POINT('Ctrl Pts',(2.37812213460139,-0.935844355601279,-6.50364407525712));
#6215=CARTESIAN_POINT('Ctrl Pts',(3.69021814608893,-1.48258393319871,-6.4245587395443));
#6216=CARTESIAN_POINT('Ctrl Pts',(4.86434964000071,-0.6831023330834,-6.34547340383148));
#6217=CARTESIAN_POINT('Ctrl Pts',(4.83469999735384,0.738068683084873,-6.26638806811864));
#6218=CARTESIAN_POINT('Ctrl Pts',(3.6274630045762,1.48794724541542,-6.18730273240583));
#6219=CARTESIAN_POINT('Ctrl Pts',(2.34041648319791,0.885466321311861,-6.108217396693));
#6220=CARTESIAN_POINT('Ctrl Pts',(2.14329602955155,-0.522012752397661,-6.02913206098017));
#6221=CARTESIAN_POINT('Ctrl Pts',(3.21538871633449,-1.45492385801227,-5.95004672526736));
#6222=CARTESIAN_POINT('Ctrl Pts',(4.58210053817705,-1.06532827696828,-5.87096138955452));
#6223=CARTESIAN_POINT('Ctrl Pts',(5.00110652655041,0.29268164606476,-5.79187605384172));
#6224=CARTESIAN_POINT('Ctrl Pts',(4.0915126774771,1.3846179768374,-5.71279071812886));
#6225=CARTESIAN_POINT('Ctrl Pts',(2.68015471140121,1.21796098890514,-5.63370538241607));
#6226=CARTESIAN_POINT('Ctrl Pts',(2.04996438291253,-0.0558969176351795,
-5.55462004670322));
#6227=CARTESIAN_POINT('Ctrl Pts',(2.77379275772401,-1.27882148436788,-5.4755347109904));
#6228=CARTESIAN_POINT('Ctrl Pts',(4.19367100293735,-1.33952390395431,-5.39644937527758));
#6229=CARTESIAN_POINT('Ctrl Pts',(5.0189224523892,-0.182127600312612,-5.31736403956475));
#6230=CARTESIAN_POINT('Ctrl Pts',(4.49937867021184,1.13992756204607,-5.23827870385193));
#6231=CARTESIAN_POINT('Ctrl Pts',(3.10732931637288,1.42753615988261,-5.15919336813911));
#6232=CARTESIAN_POINT('Ctrl Pts',(2.1080715710874,0.413950633477231,-5.08010803242628));
#6233=CARTESIAN_POINT('Ctrl Pts',(2.30975871420901,-0.507102993307459,-5.0273844752844));
#6234=CARTESIAN_POINT('Ctrl Pts',(2.58274506550209,-0.824055309621745,-5.00102269671346));
#6235=CARTESIAN_POINT('Ctrl Pts',(2.58140289770062,-0.825211298936501,-5.));
#6236=CARTESIAN_POINT('Ctrl Pts',(2.5443038685143,-0.790565736135109,-5.));
#6237=CARTESIAN_POINT('Ctrl Pts',(2.5096133001869,-0.753654963622072,-5.));
#6238=CARTESIAN_POINT('Ctrl Pts',(2.4773324300738,-0.714804509422556,-5.));
#6239=CARTESIAN_POINT('Ctrl Pts',(2.44382302669503,-0.674475499186495,-5.));
#6240=CARTESIAN_POINT('Ctrl Pts',(2.41290963390399,-0.632055844314543,-5.));
#6241=CARTESIAN_POINT('Ctrl Pts',(2.38462175988235,-0.587859965043762,-5.));
#6242=CARTESIAN_POINT('Ctrl Pts',(2.36183436288275,-0.552257818133782,-5.));
#6243=CARTESIAN_POINT('Ctrl Pts',(2.34075115345325,-0.515501897022739,-5.));
#6244=CARTESIAN_POINT('Ctrl Pts',(2.32140404015463,-0.477738428764528,-5.));
#6245=CARTESIAN_POINT('Ctrl Pts',(2.31256386104482,-0.460483357268475,-5.));
#6246=CARTESIAN_POINT('Ctrl Pts',(2.30408636388687,-0.443017739150525,-5.));
#6247=CARTESIAN_POINT('Ctrl Pts',(2.29597576406928,-0.425354688536879,-5.));
#6248=CARTESIAN_POINT('Ctrl Pts',(2.29064587076453,-0.413747387310767,-5.));
#6249=CARTESIAN_POINT('Ctrl Pts',(2.28547842331998,-0.402063202260178,-5.));
#6250=CARTESIAN_POINT('Ctrl Pts',(2.28047895461962,-0.390318443110687,-5.));
#6251=CARTESIAN_POINT('Ctrl Pts',(2.25908332594452,-0.340055801077734,-5.));
#6252=CARTESIAN_POINT('Ctrl Pts',(2.24073091648794,-0.288620954181535,-5.));
#6253=CARTESIAN_POINT('Ctrl Pts',(2.22545160263789,-0.236345852796058,-5.));
#6254=CARTESIAN_POINT('Ctrl Pts',(2.20993735019612,-0.183266956238725,-5.));
#6255=CARTESIAN_POINT('Ctrl Pts',(2.19759084383281,-0.12932081162433,-5.));
#6256=CARTESIAN_POINT('Ctrl Pts',(2.18848488354503,-0.0748214956571345,
-5.));
#6257=CARTESIAN_POINT('Ctrl Pts',(2.18251502859455,-0.039091819605201,-5.));
#6258=CARTESIAN_POINT('Ctrl Pts',(2.17793885768262,-0.00312372539428411,
-5.));
#6259=CARTESIAN_POINT('Ctrl Pts',(2.17478819450278,0.0329987838147586,-5.));
#6260=CARTESIAN_POINT('Ctrl Pts',(2.17359339586394,0.0466972093114556,-5.));
#6261=CARTESIAN_POINT('Ctrl Pts',(2.17260369603544,0.0604178640169256,-5.));
#6262=CARTESIAN_POINT('Ctrl Pts',(2.17182120172493,0.0741562274991369,-5.));
#6263=CARTESIAN_POINT('Ctrl Pts',(2.17126458820083,0.0839287700089929,-5.));
#6264=CARTESIAN_POINT('Ctrl Pts',(2.17081297188068,0.0937093000099677,-5.));
#6265=CARTESIAN_POINT('Ctrl Pts',(2.17046729064728,0.103483333436382,-5.));
#6266=CARTESIAN_POINT('Ctrl Pts',(2.16845812804063,0.160291804880593,-5.));
#6267=CARTESIAN_POINT('Ctrl Pts',(2.17001676354188,0.21699286492916,-5.));
#6268=CARTESIAN_POINT('Ctrl Pts',(2.17520064633437,0.273253460289501,-5.));
#6269=CARTESIAN_POINT('Ctrl Pts',(2.17885174648405,0.312878790638097,-5.));
#6270=CARTESIAN_POINT('Ctrl Pts',(2.18430208543024,0.352286313487869,-5.));
#6271=CARTESIAN_POINT('Ctrl Pts',(2.19158648959198,0.391364544701194,-5.));
#6272=CARTESIAN_POINT('Ctrl Pts',(2.20166270408611,0.445419842981498,-5.));
#6273=CARTESIAN_POINT('Ctrl Pts',(2.21524590860259,0.498845689754294,-5.));
#6274=CARTESIAN_POINT('Ctrl Pts',(2.23210915118275,0.55143920077537,-5.));
#6275=CARTESIAN_POINT('Ctrl Pts',(2.23674543347051,0.565898956213224,-5.));
#6276=CARTESIAN_POINT('Ctrl Pts',(2.24162995143373,0.580295763058249,-5.));
#6277=CARTESIAN_POINT('Ctrl Pts',(2.24675865344609,0.594625292699198,-5.));
#6278=CARTESIAN_POINT('Ctrl Pts',(2.25113136684655,0.606842599560134,-5.));
#6279=CARTESIAN_POINT('Ctrl Pts',(2.25568301689667,0.619014263661864,-5.));
#6280=CARTESIAN_POINT('Ctrl Pts',(2.26040126263906,0.631113161664277,-5.));
#6281=CARTESIAN_POINT('Ctrl Pts',(2.2808408613784,0.68352599343681,-5.));
#6282=CARTESIAN_POINT('Ctrl Pts',(2.30443261947429,0.734662665201017,-5.));
#6283=CARTESIAN_POINT('Ctrl Pts',(2.33089635496046,0.784320314073398,-5.));
#6284=CARTESIAN_POINT('Ctrl Pts',(2.35823540126121,0.835620432396352,-5.));
#6285=CARTESIAN_POINT('Ctrl Pts',(2.38863981713511,0.885342970150477,-5.));
#6286=CARTESIAN_POINT('Ctrl Pts',(2.42185625359725,0.933258674009797,-5.));
#6287=CARTESIAN_POINT('Ctrl Pts',(2.44276922138912,0.963426256034342,-5.));
#6288=CARTESIAN_POINT('Ctrl Pts',(2.46479795057879,0.992877467689253,-5.));
#6289=CARTESIAN_POINT('Ctrl Pts',(2.48788911204523,1.02155146193549,-5.));
#6290=CARTESIAN_POINT('Ctrl Pts',(2.49899636447663,1.03534415455392,-5.));
#6291=CARTESIAN_POINT('Ctrl Pts',(2.51034954571346,1.04895696236408,-5.));
#6292=CARTESIAN_POINT('Ctrl Pts',(2.52194327615918,1.06238276343662,-5.));
#6293=CARTESIAN_POINT('Ctrl Pts',(2.52918083973574,1.07076402512661,-5.));
#6294=CARTESIAN_POINT('Ctrl Pts',(2.53651215398541,1.07907240407868,-5.));
#6295=CARTESIAN_POINT('Ctrl Pts',(2.54393597594497,1.08730611385574,-5.));
#6296=CARTESIAN_POINT('Ctrl Pts',(2.56001623173551,1.10514061474239,-5.));
#6297=CARTESIAN_POINT('Ctrl Pts',(2.57650160603444,1.12259268997826,-5.));
#6298=CARTESIAN_POINT('Ctrl Pts',(2.59336983697945,1.13964202052506,-5.));
#6299=CARTESIAN_POINT('Ctrl Pts',(2.63584485418862,1.18257305524596,-5.));
#6300=CARTESIAN_POINT('Ctrl Pts',(2.68075393598663,1.22296307876887,-5.));
#6301=CARTESIAN_POINT('Ctrl Pts',(2.72784980179568,1.26055525794552,-5.));
#6302=CARTESIAN_POINT('Ctrl Pts',(2.75098798760318,1.27902428514687,-5.));
#6303=CARTESIAN_POINT('Ctrl Pts',(2.77465471369495,1.29681760412996,-5.));
#6304=CARTESIAN_POINT('Ctrl Pts',(2.79882434356303,1.31390198293556,-5.));
#6305=CARTESIAN_POINT('Ctrl Pts',(2.81224950241102,1.32339159864487,-5.));
#6306=CARTESIAN_POINT('Ctrl Pts',(2.82583191164499,1.33266357611002,-5.));
#6307=CARTESIAN_POINT('Ctrl Pts',(2.83954728536104,1.34169928144364,-5.));
#6308=CARTESIAN_POINT('Ctrl Pts',(2.89033718890059,1.37515973332831,-5.));
#6309=CARTESIAN_POINT('Ctrl Pts',(2.94300347308374,1.40542380145655,-5.));
#6310=CARTESIAN_POINT('Ctrl Pts',(2.99730690408547,1.43222733834652,-5.));
#6311=CARTESIAN_POINT('Ctrl Pts',(3.0285797562309,1.44766325152312,-5.));
#6312=CARTESIAN_POINT('Ctrl Pts',(3.06039632623927,1.46195091726861,-5.));
#6313=CARTESIAN_POINT('Ctrl Pts',(3.0927161721997,1.47503398848531,-5.));
#6314=CARTESIAN_POINT('Ctrl Pts',(3.10834477213784,1.48136044456614,-5.));
#6315=CARTESIAN_POINT('Ctrl Pts',(3.12409110440959,1.48740515602026,-5.));
#6316=CARTESIAN_POINT('Ctrl Pts',(3.13994823780237,1.49317013007988,-5.));
#6317=CARTESIAN_POINT('Ctrl Pts',(3.14100520856575,1.49064942821851,-6.5));
#6318=CARTESIAN_POINT('Ctrl Pts',(3.08494727205938,1.47016608894724,-6.5));
#6319=CARTESIAN_POINT('Ctrl Pts',(3.03037988871937,1.44624037846191,-6.5));
#6320=CARTESIAN_POINT('Ctrl Pts',(2.97748590856093,1.41915231489488,-6.5));
#6321=CARTESIAN_POINT('Ctrl Pts',(2.92372703313026,1.39162132118641,-6.5));
#6322=CARTESIAN_POINT('Ctrl Pts',(2.871695963559,1.36082288444892,-6.5));
#6323=CARTESIAN_POINT('Ctrl Pts',(2.82161578916584,1.32700688826385,-6.5));
#6324=CARTESIAN_POINT('Ctrl Pts',(2.77170003062915,1.29330191177955,-6.5));
#6325=CARTESIAN_POINT('Ctrl Pts',(2.72372171689141,1.25659822244747,-6.5));
#6326=CARTESIAN_POINT('Ctrl Pts',(2.67794303793286,1.21711325915177,-6.5));
#6327=CARTESIAN_POINT('Ctrl Pts',(2.6684202947039,1.20889971574195,-6.5));
#6328=CARTESIAN_POINT('Ctrl Pts',(2.65899289462306,1.20056574756288,-6.5));
#6329=CARTESIAN_POINT('Ctrl Pts',(2.64966346414571,1.19211320543645,-6.5));
#6330=CARTESIAN_POINT('Ctrl Pts',(2.64194525774896,1.18512044581758,-6.5));
#6331=CARTESIAN_POINT('Ctrl Pts',(2.63429426375662,1.17804654637327,-6.5));
#6332=CARTESIAN_POINT('Ctrl Pts',(2.62672209878259,1.17090245274249,-6.5));
#6333=CARTESIAN_POINT('Ctrl Pts',(2.58365694565614,1.13027186859452,-6.5));
#6334=CARTESIAN_POINT('Ctrl Pts',(2.54305162503511,1.08729601398087,-6.5));
#6335=CARTESIAN_POINT('Ctrl Pts',(2.50511274754567,1.04221545654921,-6.5));
#6336=CARTESIAN_POINT('Ctrl Pts',(2.46574912979395,0.995441963283155,-6.50000000000001));
#6337=CARTESIAN_POINT('Ctrl Pts',(2.42925494262276,0.946401837425422,-6.5));
#6338=CARTESIAN_POINT('Ctrl Pts',(2.39591368681376,0.89533584763873,-6.5));
#6339=CARTESIAN_POINT('Ctrl Pts',(2.36502342126014,0.84802383292922,-6.5));
#6340=CARTESIAN_POINT('Ctrl Pts',(2.33683964378032,0.798971905014553,-6.50000000000001));
#6341=CARTESIAN_POINT('Ctrl Pts',(2.31163738960224,0.74836188306999,-6.5));
#6342=CARTESIAN_POINT('Ctrl Pts',(2.30963771500258,0.744346227380796,-6.5));
#6343=CARTESIAN_POINT('Ctrl Pts',(2.30765683836007,0.740320761201582,-6.5));
#6344=CARTESIAN_POINT('Ctrl Pts',(2.30569491147364,0.736285575060568,-6.5));
#6345=CARTESIAN_POINT('Ctrl Pts',(2.30080361350804,0.726225415378344,-6.5));
#6346=CARTESIAN_POINT('Ctrl Pts',(2.29603387978872,0.716112511626207,-6.5));
#6347=CARTESIAN_POINT('Ctrl Pts',(2.29139002741425,0.70595426885953,-6.5));
#6348=CARTESIAN_POINT('Ctrl Pts',(2.26822780098137,0.655287817786391,-6.5));
#6349=CARTESIAN_POINT('Ctrl Pts',(2.24817102530427,0.603448830555026,-6.5));
#6350=CARTESIAN_POINT('Ctrl Pts',(2.23143263759802,0.550627378413331,-6.5));
#6351=CARTESIAN_POINT('Ctrl Pts',(2.21963915463869,0.513410598239972,-6.5));
#6352=CARTESIAN_POINT('Ctrl Pts',(2.20949394642941,0.475705703141791,-6.5));
#6353=CARTESIAN_POINT('Ctrl Pts',(2.20108697408611,0.437576967973437,-6.5));
#6354=CARTESIAN_POINT('Ctrl Pts',(2.1891873345697,0.383607692806106,-6.5));
#6355=CARTESIAN_POINT('Ctrl Pts',(2.18076876031134,0.328788238188614,-6.5));
#6356=CARTESIAN_POINT('Ctrl Pts',(2.17577416902111,0.273435929921917,-6.5));
#6357=CARTESIAN_POINT('Ctrl Pts',(2.17434923477101,0.257644167335565,-6.5));
#6358=CARTESIAN_POINT('Ctrl Pts',(2.17320326721325,0.241809120422912,-6.5));
#6359=CARTESIAN_POINT('Ctrl Pts',(2.17233558451626,0.225938418974115,-6.5));
#6360=CARTESIAN_POINT('Ctrl Pts',(2.17166526676672,0.213677700953913,-6.5));
#6361=CARTESIAN_POINT('Ctrl Pts',(2.17116110529721,0.201393005178454,-6.5));
#6362=CARTESIAN_POINT('Ctrl Pts',(2.17082312577695,0.189111602497678,-6.5));
#6363=CARTESIAN_POINT('Ctrl Pts',(2.16929543448595,0.133598795384436,-6.5));
#6364=CARTESIAN_POINT('Ctrl Pts',(2.17115162578008,0.0780521664174741,-6.5));
#6365=CARTESIAN_POINT('Ctrl Pts',(2.17628380677392,0.0227871693634732,-6.5));
#6366=CARTESIAN_POINT('Ctrl Pts',(2.18141533505767,-0.0324707990956518,
-6.5));
#6367=CARTESIAN_POINT('Ctrl Pts',(2.18982247496828,-0.0874483413955667,
-6.5));
#6368=CARTESIAN_POINT('Ctrl Pts',(2.20144629520756,-0.141815029635975,-6.5));
#6369=CARTESIAN_POINT('Ctrl Pts',(2.20865289933067,-0.175521607298768,-6.5));
#6370=CARTESIAN_POINT('Ctrl Pts',(2.21709687600562,-0.208993018190762,-6.5));
#6371=CARTESIAN_POINT('Ctrl Pts',(2.22677248421428,-0.24214473226519,-6.5));
#6372=CARTESIAN_POINT('Ctrl Pts',(2.23175694861537,-0.259223094170246,-6.5));
#6373=CARTESIAN_POINT('Ctrl Pts',(2.23706837039207,-0.276216526665636,-6.5));
#6374=CARTESIAN_POINT('Ctrl Pts',(2.24270655913964,-0.293112851925979,-6.5));
#6375=CARTESIAN_POINT('Ctrl Pts',(2.24692178219473,-0.305744883766785,-6.5));
#6376=CARTESIAN_POINT('Ctrl Pts',(2.25132049507297,-0.318324481904199,-6.5));
#6377=CARTESIAN_POINT('Ctrl Pts',(2.25589478335012,-0.330825919503712,-6.5));
#6378=CARTESIAN_POINT('Ctrl Pts',(2.2743421029172,-0.381242071803956,-6.5));
#6379=CARTESIAN_POINT('Ctrl Pts',(2.29566569186883,-0.4304646756,-6.5));
#6380=CARTESIAN_POINT('Ctrl Pts',(2.31982030634388,-0.478178835899828,-6.5));
#6381=CARTESIAN_POINT('Ctrl Pts',(2.3360728938977,-0.510283615242568,-6.5));
#6382=CARTESIAN_POINT('Ctrl Pts',(2.35360804649871,-0.541704938378982,-6.5));
#6383=CARTESIAN_POINT('Ctrl Pts',(2.3724212135575,-0.572337190454871,-6.5));
#6384=CARTESIAN_POINT('Ctrl Pts',(2.3809158305163,-0.58616842084565,-6.49999999999999));
#6385=CARTESIAN_POINT('Ctrl Pts',(2.38967347678636,-0.599841872207131,-6.5));
#6386=CARTESIAN_POINT('Ctrl Pts',(2.39867859342135,-0.613324895247866,-6.5));
#6387=CARTESIAN_POINT('Ctrl Pts',(2.42713371190609,-0.655929675808517,-6.5));
#6388=CARTESIAN_POINT('Ctrl Pts',(2.45808277339633,-0.696680211491728,-6.49999999999999));
#6389=CARTESIAN_POINT('Ctrl Pts',(2.49150132174337,-0.735275360483379,-6.5));
#6390=CARTESIAN_POINT('Ctrl Pts',(2.51006349039157,-0.756712846550875,-6.5));
#6391=CARTESIAN_POINT('Ctrl Pts',(2.5293881120533,-0.77748468706277,-6.5));
#6392=CARTESIAN_POINT('Ctrl Pts',(2.54947484834281,-0.797533396503153,-6.5));
#6393=CARTESIAN_POINT('Ctrl Pts',(2.55933167690434,-0.807371564784229,-6.5));
#6394=CARTESIAN_POINT('Ctrl Pts',(2.56937206717339,-0.817035528308793,-6.5));
#6395=CARTESIAN_POINT('Ctrl Pts',(2.579590276763,-0.826522883252263,-6.5));
#6396=CARTESIAN_POINT('Origin',(3.53951905042299,5.55111512312578E-16,-6.5));
#6397=CARTESIAN_POINT('',(2.38481851204374,2.,-6.5));
#6398=CARTESIAN_POINT('',(4.69421958880225,2.,-6.5));
#6399=CARTESIAN_POINT('',(2.38481851204374,2.,-6.5));
#6400=CARTESIAN_POINT('',(5.8489201271815,1.94289029309402E-15,-6.5));
#6401=CARTESIAN_POINT('',(4.69421958880225,2.,-6.5));
#6402=CARTESIAN_POINT('',(4.69421958880225,-2.,-6.5));
#6403=CARTESIAN_POINT('',(5.8489201271815,1.94289029309402E-15,-6.5));
#6404=CARTESIAN_POINT('',(2.38481851204374,-2.,-6.5));
#6405=CARTESIAN_POINT('',(4.69421958880225,-2.,-6.5));
#6406=CARTESIAN_POINT('',(1.23011797366449,-1.2490009027033E-15,-6.5));
#6407=CARTESIAN_POINT('',(2.38481851204374,-2.,-6.5));
#6408=CARTESIAN_POINT('',(1.23011797366449,-1.2490009027033E-15,-6.5));
#6409=CARTESIAN_POINT('Origin',(5.8489201271815,1.94289029309402E-15,-6.5));
#6410=CARTESIAN_POINT('',(4.69421958880225,2.,-5.));
#6411=CARTESIAN_POINT('',(4.69421958880225,2.,-6.5));
#6412=CARTESIAN_POINT('',(5.8489201271815,1.94289029309402E-15,-5.));
#6413=CARTESIAN_POINT('',(4.69421958880225,2.,-5.));
#6414=CARTESIAN_POINT('',(5.8489201271815,1.94289029309402E-15,-6.5));
#6415=CARTESIAN_POINT('Origin',(4.69421958880225,-2.,-6.5));
#6416=CARTESIAN_POINT('',(4.69421958880225,-2.,-5.));
#6417=CARTESIAN_POINT('',(5.8489201271815,1.94289029309402E-15,-5.));
#6418=CARTESIAN_POINT('',(4.69421958880225,-2.,-6.5));
#6419=CARTESIAN_POINT('Origin',(2.38481851204374,-2.,-6.5));
#6420=CARTESIAN_POINT('',(2.38481851204374,-2.,-5.));
#6421=CARTESIAN_POINT('',(4.69421958880225,-2.,-5.));
#6422=CARTESIAN_POINT('',(2.38481851204374,-2.,-6.5));
#6423=CARTESIAN_POINT('Origin',(1.23011797366449,-1.38777878078145E-15,
-6.5));
#6424=CARTESIAN_POINT('',(1.23011797366449,-1.2490009027033E-15,-5.));
#6425=CARTESIAN_POINT('',(2.38481851204374,-2.,-5.));
#6426=CARTESIAN_POINT('',(1.23011797366449,-1.2490009027033E-15,-6.5));
#6427=CARTESIAN_POINT('Origin',(2.38481851204374,2.,-6.5));
#6428=CARTESIAN_POINT('',(2.38481851204374,2.,-5.));
#6429=CARTESIAN_POINT('',(1.23011797366449,-1.2490009027033E-15,-5.));
#6430=CARTESIAN_POINT('',(2.38481851204374,2.,-6.5));
#6431=CARTESIAN_POINT('Origin',(4.69421958880225,2.,-6.5));
#6432=CARTESIAN_POINT('',(2.38481851204374,2.,-5.));
#6433=CARTESIAN_POINT('Origin',(3.53951905042299,5.55111512312578E-16,-5.));
#40718=UNCERTAINTY_MEASURE_WITH_UNIT(LENGTH_MEASURE(0.01),#40735,
'DISTANCE_ACCURACY_VALUE',
'Maximum model space distance between geometric entities at asserted c
onnectivities');
#40724=UNCERTAINTY_MEASURE_WITH_UNIT(LENGTH_MEASURE(0.01),#40735,
'DISTANCE_ACCURACY_VALUE',
'Maximum model space distance between geometric entities at asserted c
onnectivities');
#40728=(
GEOMETRIC_REPRESENTATION_CONTEXT(3)
GLOBAL_UNCERTAINTY_ASSIGNED_CONTEXT((#40718))
GLOBAL_UNIT_ASSIGNED_CONTEXT((#40735,#40737,#40738))
REPRESENTATION_CONTEXT('','3D')
);
#40734=(
GEOMETRIC_REPRESENTATION_CONTEXT(3)
GLOBAL_UNCERTAINTY_ASSIGNED_CONTEXT((#40724))
GLOBAL_UNIT_ASSIGNED_CONTEXT((#40735,#40737,#40738))
REPRESENTATION_CONTEXT('','3D')
);
#40735=(
LENGTH_UNIT()
NAMED_UNIT(*)
SI_UNIT(.MILLI.,.METRE.)
);
#40737=(
NAMED_UNIT(*)
PLANE_ANGLE_UNIT()
SI_UNIT($,.RADIAN.)
);
#40738=(
NAMED_UNIT(*)
SI_UNIT($,.STERADIAN.)
SOLID_ANGLE_UNIT()
);
#40742=SHAPE_DEFINITION_REPRESENTATION(#40751,#40768);
#40751=PRODUCT_DEFINITION_SHAPE('',$,#40778);
#40768=SHAPE_REPRESENTATION('',(#3299),#40728);
#40774=PRODUCT_DEFINITION_CONTEXT('part definition',#40803,'design');
#40778=PRODUCT_DEFINITION('Nut','Nut',#40787,#40774);
#40787=PRODUCT_DEFINITION_FORMATION('',$,#40808);
#40803=APPLICATION_CONTEXT(
'Core Data for Automotive Mechanical Design Process');
#40804=PRODUCT_CONTEXT('part definition',#40803,'mechanical');
#40808=PRODUCT('Nut','Nut',$,(#40804));
#40815=PRESENTATION_STYLE_ASSIGNMENT((#40818));
#40818=SURFACE_STYLE_USAGE(.BOTH.,#40821);
#40821=SURFACE_SIDE_STYLE('',(#40824));
#40824=SURFACE_STYLE_FILL_AREA(#40827);
#40827=FILL_AREA_STYLE('Opaque(203,203,203)',(#40830));
#40830=FILL_AREA_STYLE_COLOUR('Opaque(203,203,203)',#40833);
#40833=COLOUR_RGB('Opaque(203,203,203)', 0.09019608, 0.27058824, 0.51372549);
ENDSEC;
END-ISO-10303-21;
